ISO-10303-21;
HEADER;
/* Generated by software containing ST-Developer
 * from STEP Tools, Inc. (www.steptools.com) 
 */

FILE_DESCRIPTION(
/* description */ ('Hand-crank flanged shaft unit'),
/* implementation_level */ '2;1');

FILE_NAME(
/* name */ 'Handwheel - 100 mm Diameter, 12 mm Bore.step',
/* time_stamp */ '2026-10-27T18:35:45-07:00',
/* author */ (''),
/* organization */ (''),
/* preprocessor_version */ 'ST-DEVELOPER v20.2',
/* originating_system */ 'Autodesk Translation Framework v15.17.0.0',
/* authorisation */ '');

FILE_SCHEMA (('AUTOMOTIVE_DESIGN { 1 0 10303 214 3 1 1 }'));
ENDSEC;

DATA;
#10=MECHANICAL_DESIGN_GEOMETRIC_PRESENTATION_REPRESENTATION('',(#295),#6805);
#11=TOROIDAL_SURFACE('',#3848,4.4,0.6);
#213=B_SPLINE_CURVE_WITH_KNOTS('',3,(#5976,#5977,#5978,#5979,#5980,#5981,
#5982,#5983,#5984,#5985,#5986,#5987,#5988,#5989,#5990,#5991),
 .UNSPECIFIED.,.F.,.F.,(4,2,2,2,2,2,2,4),(-2.59552719332688,-2.57866585978924,
-2.54045071895435,-2.48749500888924,-2.3744647112323,-2.21556033801692,
-2.06580308432295,-1.95647920002804),.UNSPECIFIED.);
#214=B_SPLINE_CURVE_WITH_KNOTS('',3,(#5992,#5993,#5994,#5995,#5996,#5997,
#5998,#5999,#6000,#6001,#6002,#6003,#6004,#6005,#6006,#6007,#6008,#6009,
#6010,#6011,#6012,#6013,#6014,#6015,#6016,#6017,#6018,#6019,#6020,#6021,
#6022,#6023,#6024,#6025,#6026,#6027,#6028,#6029,#6030,#6031),
 .UNSPECIFIED.,.F.,.F.,(4,2,2,2,2,2,2,2,2,2,2,2,2,2,2,2,2,2,2,4),(-1.95647920002804,
-1.94940399731571,-1.82274564275395,-1.66864682416849,-1.54169125534598,
-1.43387376529483,-1.38209306412146,-1.34424705617005,-1.30493332486279,
-1.2460037370214,-1.10178537420969,-0.937426671253584,-0.78794048589305,
-0.665122735561945,-0.534841035694231,-0.375845726164312,-0.235011648675127,
-0.128548815843694,-0.0452999297674013,0.),.UNSPECIFIED.);
#215=B_SPLINE_CURVE_WITH_KNOTS('',3,(#6035,#6036,#6037,#6038,#6039,#6040,
#6041,#6042,#6043,#6044,#6045,#6046,#6047,#6048,#6049,#6050,#6051,#6052,
#6053,#6054,#6055,#6056,#6057,#6058,#6059,#6060,#6061,#6062,#6063,#6064,
#6065,#6066,#6067,#6068,#6069,#6070,#6071,#6072,#6073,#6074),
 .UNSPECIFIED.,.F.,.F.,(4,2,2,2,2,2,2,2,2,2,2,2,2,2,2,2,2,2,2,4),(-2.54361034519536,
-2.54253046486639,-2.4968571438888,-2.41437075183371,-2.26714492660274,
-2.09453621901679,-1.96116992397976,-1.84022994403498,-1.7037233477047,
-1.55334846612811,-1.42769894285765,-1.31373188966584,-1.26191388559973,
-1.22542262952322,-1.18873619849312,-1.1358415785305,-1.01347695720179,
-0.85748048653537,-0.726532050447263,-0.647957499864814),.UNSPECIFIED.);
#216=B_SPLINE_CURVE_WITH_KNOTS('',3,(#6075,#6076,#6077,#6078,#6079,#6080,
#6081,#6082,#6083,#6084,#6085,#6086,#6087,#6088,#6089,#6090),
 .UNSPECIFIED.,.F.,.F.,(4,2,2,2,2,2,2,4),(-0.647957499864814,-0.616035464948488,
-0.481588413072267,-0.322224684302864,-0.16030015410164,-0.0820369314872885,
-0.0377273936823807,0.),.UNSPECIFIED.);
#217=B_SPLINE_CURVE_WITH_KNOTS('',3,(#6094,#6095,#6096,#6097,#6098,#6099,
#6100,#6101,#6102,#6103,#6104,#6105,#6106,#6107,#6108,#6109,#6110,#6111),
 .UNSPECIFIED.,.F.,.F.,(4,2,2,2,2,2,2,2,4),(0.,0.0961983484640422,0.192396696928084,
0.28847519841324,0.384553699898396,0.480632201383552,0.576710702868707,
0.672909051332749,0.769107399796792),.UNSPECIFIED.);
#218=B_SPLINE_CURVE_WITH_KNOTS('',3,(#6112,#6113,#6114,#6115,#6116,#6117,
#6118,#6119,#6120,#6121,#6122,#6123,#6124,#6125,#6126,#6127,#6128,#6129),
 .UNSPECIFIED.,.F.,.F.,(4,2,2,2,2,2,2,2,4),(0.769107399796792,0.865305748260834,
0.961504096724876,1.05758259821003,1.15366109969519,1.24973960118034,1.3458181026655,
1.44201645112954,1.53821479959358),.UNSPECIFIED.);
#219=B_SPLINE_CURVE_WITH_KNOTS('',3,(#6133,#6134,#6135,#6136,#6137,#6138,
#6139,#6140,#6141,#6142),.UNSPECIFIED.,.F.,.F.,(4,2,2,2,4),(0.380002694880465,
0.475002363724097,0.570002032567729,0.66500371116433,0.760005389760931),
 .UNSPECIFIED.);
#220=B_SPLINE_CURVE_WITH_KNOTS('',3,(#6144,#6145,#6146,#6147,#6148,#6149,
#6150,#6151,#6152,#6153),.UNSPECIFIED.,.F.,.F.,(4,2,2,2,4),(0.,0.0950016785966008,
0.190003357193202,0.285003026036833,0.380002694880465),.UNSPECIFIED.);
#221=B_SPLINE_CURVE_WITH_KNOTS('',3,(#6155,#6156,#6157,#6158,#6159,#6160,
#6161,#6162,#6163,#6164),.UNSPECIFIED.,.F.,.F.,(4,2,2,2,4),(1.1400080846414,
1.23500775348503,1.33000742232866,1.42500910092526,1.52001077952186),
 .UNSPECIFIED.);
#222=B_SPLINE_CURVE_WITH_KNOTS('',3,(#6165,#6166,#6167,#6168,#6169,#6170,
#6171,#6172,#6173,#6174),.UNSPECIFIED.,.F.,.F.,(4,2,2,2,4),(0.760005389760931,
0.855007068357531,0.950008746954132,1.04500841579776,1.1400080846414),
 .UNSPECIFIED.);
#223=B_SPLINE_CURVE_WITH_KNOTS('',3,(#6205,#6206,#6207,#6208,#6209,#6210,
#6211,#6212,#6213,#6214,#6215,#6216,#6217,#6218),.UNSPECIFIED.,.F.,.F.,
(4,2,2,2,2,2,4),(-2.54850355944817,-2.47147966009112,-2.35116278368337,
-2.17207383157567,-2.03290678540533,-1.91210887606818,-1.90533893688978),
 .UNSPECIFIED.);
#224=B_SPLINE_CURVE_WITH_KNOTS('',3,(#6220,#6221,#6222,#6223,#6224,#6225,
#6226,#6227,#6228,#6229,#6230,#6231),.UNSPECIFIED.,.F.,.F.,(4,2,2,2,2,4),
(-0.637276313354589,-0.528249228810808,-0.380873908763749,-0.202177241884586,
-0.0799314225938296,0.),.UNSPECIFIED.);
#225=B_SPLINE_CURVE_WITH_KNOTS('',3,(#6234,#6235,#6236,#6237,#6238,#6239,
#6240,#6241,#6242,#6243,#6244,#6245,#6246,#6247,#6248,#6249,#6250,#6251,
#6252,#6253,#6254,#6255,#6256,#6257,#6258,#6259,#6260,#6261,#6262,#6263,
#6264,#6265,#6266,#6267),.UNSPECIFIED.,.T.,.F.,(4,2,2,2,2,2,2,2,2,2,2,2,
2,2,2,2,4),(0.,0.151379292814069,0.302758585628139,0.454116712920023,0.605474840211907,
0.756832967503791,0.908191094795676,1.05957038760974,1.21094968042381,1.36232897323788,
1.51370826605195,1.66506639334384,1.81642452063572,1.96778264792761,2.11914077521949,
2.27052006803356,2.42189936084763),.UNSPECIFIED.);
#226=B_SPLINE_CURVE_WITH_KNOTS('',3,(#6268,#6269,#6270,#6271,#6272,#6273,
#6274,#6275,#6276,#6277,#6278,#6279,#6280,#6281,#6282,#6283,#6284,#6285,
#6286,#6287,#6288,#6289,#6290,#6291),.UNSPECIFIED.,.F.,.F.,(4,2,2,2,2,2,
2,2,2,2,2,4),(-1.90533893688978,-1.78642522838365,-1.63371704918402,-1.47883830887698,
-1.3527241089287,-1.27308869766128,-1.19599240460016,-1.08166165023207,
-0.90752604130311,-0.769338857038376,-0.650696729228082,-0.637276313354589),
 .UNSPECIFIED.);
#227=B_SPLINE_CURVE_WITH_KNOTS('',3,(#6295,#6296,#6297,#6298,#6299,#6300,
#6301,#6302,#6303,#6304,#6305,#6306,#6307,#6308),.UNSPECIFIED.,.F.,.F.,
(4,2,2,2,2,2,4),(-2.5485035594474,-2.47147966009035,-2.35116278368264,-2.17207383157505,
-2.0329067854048,-1.91210887606772,-1.90533893688933),.UNSPECIFIED.);
#228=B_SPLINE_CURVE_WITH_KNOTS('',3,(#6310,#6311,#6312,#6313,#6314,#6315,
#6316,#6317,#6318,#6319,#6320,#6321),.UNSPECIFIED.,.F.,.F.,(4,2,2,2,2,4),
(-0.637276313354588,-0.528249228810783,-0.380873908763716,-0.202177241884562,
-0.0799314225938254,0.),.UNSPECIFIED.);
#229=B_SPLINE_CURVE_WITH_KNOTS('',3,(#6324,#6325,#6326,#6327,#6328,#6329,
#6330,#6331,#6332,#6333,#6334,#6335,#6336,#6337,#6338,#6339,#6340,#6341,
#6342,#6343,#6344,#6345,#6346,#6347,#6348,#6349,#6350,#6351,#6352,#6353,
#6354,#6355,#6356,#6357),.UNSPECIFIED.,.T.,.F.,(4,2,2,2,2,2,2,2,2,2,2,2,
2,2,2,2,4),(0.,0.151379292814069,0.302758585628139,0.454116712920023,0.605474840211907,
0.756832967503791,0.908191094795675,1.05957038760974,1.21094968042381,1.36232897323788,
1.51370826605195,1.66506639334384,1.81642452063572,1.9677826479276,2.11914077521949,
2.27052006803356,2.42189936084763),.UNSPECIFIED.);
#230=B_SPLINE_CURVE_WITH_KNOTS('',3,(#6358,#6359,#6360,#6361,#6362,#6363,
#6364,#6365,#6366,#6367,#6368,#6369,#6370,#6371,#6372,#6373,#6374,#6375,
#6376,#6377,#6378,#6379,#6380,#6381),.UNSPECIFIED.,.F.,.F.,(4,2,2,2,2,2,
2,2,2,2,2,4),(-1.90533893688933,-1.78642522838326,-1.63371704918372,-1.47883830887675,
-1.35272410892854,-1.27308869766117,-1.1959924046001,-1.08166165023206,
-0.907526041303146,-0.7693388570384,-0.65069672922808,-0.637276313354588),
 .UNSPECIFIED.);
#231=B_SPLINE_CURVE_WITH_KNOTS('',3,(#6385,#6386,#6387,#6388,#6389,#6390,
#6391,#6392,#6393,#6394,#6395,#6396),.UNSPECIFIED.,.F.,.F.,(4,2,2,2,2,4),
(-2.61916424636074,-2.54165598774645,-2.39715438567385,-2.22985321946239,
-2.07412217165227,-1.96431456403181),.UNSPECIFIED.);
#232=B_SPLINE_CURVE_WITH_KNOTS('',3,(#6398,#6399,#6400,#6401,#6402,#6403,
#6404,#6405,#6406,#6407,#6408,#6409),.UNSPECIFIED.,.F.,.F.,(4,2,2,2,2,4),
(-0.649106074577762,-0.568991182312238,-0.428137419269516,-0.24870582271537,
-0.112671421215055,0.),.UNSPECIFIED.);
#233=B_SPLINE_CURVE_WITH_KNOTS('',3,(#6412,#6413,#6414,#6415,#6416,#6417,
#6418,#6419,#6420,#6421,#6422,#6423,#6424,#6425,#6426,#6427,#6428,#6429,
#6430,#6431,#6432,#6433,#6434,#6435,#6436,#6437,#6438,#6439,#6440,#6441,
#6442,#6443,#6444,#6445),.UNSPECIFIED.,.T.,.F.,(4,2,2,2,2,2,2,2,2,2,2,2,
2,2,2,2,4),(0.,0.151379292814069,0.302758585628139,0.454116712920023,0.605474840211907,
0.756832967503791,0.908191094795675,1.05957038760974,1.21094968042381,1.36232897323788,
1.51370826605195,1.66506639334384,1.81642452063572,1.96778264792761,2.11914077521949,
2.27052006803356,2.42189936084763),.UNSPECIFIED.);
#234=B_SPLINE_CURVE_WITH_KNOTS('',3,(#6446,#6447,#6448,#6449,#6450,#6451,
#6452,#6453,#6454,#6455,#6456,#6457,#6458,#6459,#6460,#6461,#6462,#6463,
#6464,#6465,#6466,#6467,#6468,#6469),.UNSPECIFIED.,.F.,.F.,(4,2,2,2,2,2,
2,2,2,2,2,4),(-1.96431456403181,-1.95510446892338,-1.83271225668806,-1.67410879488211,
-1.50389075900942,-1.37768596650605,-1.25930643549399,-1.12433269575576,
-0.949014691445703,-0.810038710964932,-0.682802605332806,-0.649106074577762),
 .UNSPECIFIED.);
#254=SHAPE_REPRESENTATION_RELATIONSHIP('SRR','None',#6916,#274);
#274=ADVANCED_BREP_SHAPE_REPRESENTATION('',(#315),#6799);
#295=STYLED_ITEM('',(#7084),#315);
#315=MANIFOLD_SOLID_BREP('Body1',#3337);
#396=FACE_BOUND('',#915,.T.);
#397=FACE_BOUND('',#917,.T.);
#398=FACE_BOUND('',#922,.T.);
#399=FACE_BOUND('',#924,.T.);
#400=FACE_BOUND('',#925,.T.);
#401=FACE_BOUND('',#926,.T.);
#402=FACE_BOUND('',#928,.T.);
#403=FACE_BOUND('',#929,.T.);
#482=PLANE('',#3834);
#483=PLANE('',#3835);
#484=PLANE('',#3836);
#485=PLANE('',#3837);
#486=PLANE('',#3845);
#645=FACE_OUTER_BOUND('',#909,.T.);
#646=FACE_OUTER_BOUND('',#910,.T.);
#647=FACE_OUTER_BOUND('',#911,.T.);
#648=FACE_OUTER_BOUND('',#912,.T.);
#649=FACE_OUTER_BOUND('',#913,.T.);
#650=FACE_OUTER_BOUND('',#914,.T.);
#651=FACE_OUTER_BOUND('',#916,.T.);
#652=FACE_OUTER_BOUND('',#918,.T.);
#653=FACE_OUTER_BOUND('',#919,.T.);
#654=FACE_OUTER_BOUND('',#920,.T.);
#655=FACE_OUTER_BOUND('',#921,.T.);
#656=FACE_OUTER_BOUND('',#923,.T.);
#657=FACE_OUTER_BOUND('',#927,.T.);
#909=EDGE_LOOP('',(#2789,#2790,#2791,#2792,#2793,#2794));
#910=EDGE_LOOP('',(#2795,#2796,#2797,#2798,#2799,#2800,#2801,#2802));
#911=EDGE_LOOP('',(#2803,#2804,#2805,#2806));
#912=EDGE_LOOP('',(#2807,#2808,#2809,#2810));
#913=EDGE_LOOP('',(#2811,#2812,#2813,#2814));
#914=EDGE_LOOP('',(#2815));
#915=EDGE_LOOP('',(#2816,#2817,#2818,#2819));
#916=EDGE_LOOP('',(#2820,#2821,#2822,#2823));
#917=EDGE_LOOP('',(#2824,#2825));
#918=EDGE_LOOP('',(#2826,#2827,#2828,#2829,#2830,#2831));
#919=EDGE_LOOP('',(#2832,#2833,#2834,#2835,#2836,#2837));
#920=EDGE_LOOP('',(#2838,#2839,#2840,#2841,#2842,#2843));
#921=EDGE_LOOP('',(#2844));
#922=EDGE_LOOP('',(#2845,#2846,#2847,#2848));
#923=EDGE_LOOP('',(#2849,#2850,#2851,#2852,#2853,#2854,#2855,#2856,#2857,
#2858));
#924=EDGE_LOOP('',(#2859));
#925=EDGE_LOOP('',(#2860));
#926=EDGE_LOOP('',(#2861));
#927=EDGE_LOOP('',(#2862,#2863,#2864,#2865,#2866,#2867,#2868,#2869,#2870,
#2871,#2872,#2873,#2874,#2875,#2876,#2877,#2878,#2879,#2880));
#928=EDGE_LOOP('',(#2881,#2882));
#929=EDGE_LOOP('',(#2883,#2884));
#1125=LINE('',#6033,#1353);
#1126=LINE('',#6131,#1354);
#1127=LINE('',#6178,#1355);
#1128=LINE('',#6180,#1356);
#1129=LINE('',#6182,#1357);
#1130=LINE('',#6183,#1358);
#1131=LINE('',#6187,#1359);
#1132=LINE('',#6189,#1360);
#1133=LINE('',#6191,#1361);
#1134=LINE('',#6192,#1362);
#1135=LINE('',#6194,#1363);
#1136=LINE('',#6195,#1364);
#1137=LINE('',#6233,#1365);
#1138=LINE('',#6323,#1366);
#1139=LINE('',#6411,#1367);
#1140=LINE('',#6474,#1368);
#1141=LINE('',#6475,#1369);
#1353=VECTOR('',#4642,0.4);
#1354=VECTOR('',#4645,0.25);
#1355=VECTOR('',#4648,1.);
#1356=VECTOR('',#4649,1.);
#1357=VECTOR('',#4650,1.);
#1358=VECTOR('',#4651,1.);
#1359=VECTOR('',#4654,1.);
#1360=VECTOR('',#4655,1.);
#1361=VECTOR('',#4656,1.);
#1362=VECTOR('',#4657,1.);
#1363=VECTOR('',#4660,1.);
#1364=VECTOR('',#4661,1.);
#1365=VECTOR('',#4674,0.4);
#1366=VECTOR('',#4677,0.4);
#1367=VECTOR('',#4680,0.4);
#1368=VECTOR('',#4687,1.6);
#1369=VECTOR('',#4688,1.6);
#1538=CIRCLE('',#3838,1.6);
#1539=CIRCLE('',#3839,0.6);
#1540=CIRCLE('',#3841,0.6);
#1541=CIRCLE('',#3846,1.6);
#1542=CIRCLE('',#3849,0.6);
#1543=CIRCLE('',#3850,3.8);
#1544=CIRCLE('',#3851,3.8);
#1545=CIRCLE('',#3852,3.8);
#1546=CIRCLE('',#3853,3.8);
#1754=VERTEX_POINT('',#5974);
#1755=VERTEX_POINT('',#5975);
#1756=VERTEX_POINT('',#6032);
#1757=VERTEX_POINT('',#6034);
#1758=VERTEX_POINT('',#6092);
#1759=VERTEX_POINT('',#6093);
#1760=VERTEX_POINT('',#6130);
#1761=VERTEX_POINT('',#6132);
#1762=VERTEX_POINT('',#6143);
#1763=VERTEX_POINT('',#6154);
#1764=VERTEX_POINT('',#6176);
#1765=VERTEX_POINT('',#6177);
#1766=VERTEX_POINT('',#6179);
#1767=VERTEX_POINT('',#6181);
#1768=VERTEX_POINT('',#6185);
#1769=VERTEX_POINT('',#6186);
#1770=VERTEX_POINT('',#6188);
#1771=VERTEX_POINT('',#6190);
#1772=VERTEX_POINT('',#6197);
#1773=VERTEX_POINT('',#6203);
#1774=VERTEX_POINT('',#6204);
#1775=VERTEX_POINT('',#6219);
#1776=VERTEX_POINT('',#6232);
#1777=VERTEX_POINT('',#6293);
#1778=VERTEX_POINT('',#6294);
#1779=VERTEX_POINT('',#6309);
#1780=VERTEX_POINT('',#6322);
#1781=VERTEX_POINT('',#6383);
#1782=VERTEX_POINT('',#6384);
#1783=VERTEX_POINT('',#6397);
#1784=VERTEX_POINT('',#6410);
#1785=VERTEX_POINT('',#6471);
#1786=VERTEX_POINT('',#6477);
#2112=EDGE_CURVE('',#1754,#1755,#213,.T.);
#2113=EDGE_CURVE('',#1755,#1754,#214,.T.);
#2114=EDGE_CURVE('',#1755,#1756,#1125,.T.);
#2115=EDGE_CURVE('',#1757,#1756,#215,.T.);
#2116=EDGE_CURVE('',#1756,#1757,#216,.T.);
#2117=EDGE_CURVE('',#1758,#1759,#217,.T.);
#2118=EDGE_CURVE('',#1759,#1758,#218,.T.);
#2119=EDGE_CURVE('',#1759,#1760,#1126,.T.);
#2120=EDGE_CURVE('',#1761,#1760,#219,.T.);
#2121=EDGE_CURVE('',#1762,#1761,#220,.T.);
#2122=EDGE_CURVE('',#1763,#1762,#221,.T.);
#2123=EDGE_CURVE('',#1760,#1763,#222,.T.);
#2124=EDGE_CURVE('',#1764,#1765,#1127,.T.);
#2125=EDGE_CURVE('',#1764,#1766,#1128,.T.);
#2126=EDGE_CURVE('',#1767,#1766,#1129,.T.);
#2127=EDGE_CURVE('',#1765,#1767,#1130,.T.);
#2128=EDGE_CURVE('',#1768,#1769,#1131,.T.);
#2129=EDGE_CURVE('',#1770,#1768,#1132,.T.);
#2130=EDGE_CURVE('',#1771,#1770,#1133,.T.);
#2131=EDGE_CURVE('',#1771,#1769,#1134,.T.);
#2132=EDGE_CURVE('',#1769,#1764,#1135,.T.);
#2133=EDGE_CURVE('',#1766,#1771,#1136,.T.);
#2134=EDGE_CURVE('',#1772,#1772,#1538,.T.);
#2135=EDGE_CURVE('',#1767,#1770,#1539,.T.);
#2136=EDGE_CURVE('',#1765,#1768,#1540,.T.);
#2137=EDGE_CURVE('',#1773,#1774,#223,.T.);
#2138=EDGE_CURVE('',#1775,#1773,#224,.T.);
#2139=EDGE_CURVE('',#1775,#1776,#1137,.T.);
#2140=EDGE_CURVE('',#1776,#1776,#225,.T.);
#2141=EDGE_CURVE('',#1774,#1775,#226,.T.);
#2142=EDGE_CURVE('',#1777,#1778,#227,.T.);
#2143=EDGE_CURVE('',#1779,#1777,#228,.T.);
#2144=EDGE_CURVE('',#1779,#1780,#1138,.T.);
#2145=EDGE_CURVE('',#1780,#1780,#229,.T.);
#2146=EDGE_CURVE('',#1778,#1779,#230,.T.);
#2147=EDGE_CURVE('',#1781,#1782,#231,.T.);
#2148=EDGE_CURVE('',#1783,#1781,#232,.T.);
#2149=EDGE_CURVE('',#1783,#1784,#1139,.T.);
#2150=EDGE_CURVE('',#1784,#1784,#233,.T.);
#2151=EDGE_CURVE('',#1782,#1783,#234,.T.);
#2152=EDGE_CURVE('',#1785,#1785,#1541,.T.);
#2153=EDGE_CURVE('',#1772,#1763,#1140,.T.);
#2154=EDGE_CURVE('',#1761,#1785,#1141,.T.);
#2155=EDGE_CURVE('',#1786,#1786,#1542,.T.);
#2156=EDGE_CURVE('',#1774,#1786,#1543,.T.);
#2157=EDGE_CURVE('',#1778,#1775,#1544,.T.);
#2158=EDGE_CURVE('',#1782,#1779,#1545,.T.);
#2159=EDGE_CURVE('',#1786,#1783,#1546,.T.);
#2789=ORIENTED_EDGE('',*,*,#2112,.F.);
#2790=ORIENTED_EDGE('',*,*,#2113,.F.);
#2791=ORIENTED_EDGE('',*,*,#2114,.T.);
#2792=ORIENTED_EDGE('',*,*,#2115,.F.);
#2793=ORIENTED_EDGE('',*,*,#2116,.F.);
#2794=ORIENTED_EDGE('',*,*,#2114,.F.);
#2795=ORIENTED_EDGE('',*,*,#2117,.F.);
#2796=ORIENTED_EDGE('',*,*,#2118,.F.);
#2797=ORIENTED_EDGE('',*,*,#2119,.T.);
#2798=ORIENTED_EDGE('',*,*,#2120,.F.);
#2799=ORIENTED_EDGE('',*,*,#2121,.F.);
#2800=ORIENTED_EDGE('',*,*,#2122,.F.);
#2801=ORIENTED_EDGE('',*,*,#2123,.F.);
#2802=ORIENTED_EDGE('',*,*,#2119,.F.);
#2803=ORIENTED_EDGE('',*,*,#2124,.F.);
#2804=ORIENTED_EDGE('',*,*,#2125,.T.);
#2805=ORIENTED_EDGE('',*,*,#2126,.F.);
#2806=ORIENTED_EDGE('',*,*,#2127,.F.);
#2807=ORIENTED_EDGE('',*,*,#2128,.F.);
#2808=ORIENTED_EDGE('',*,*,#2129,.F.);
#2809=ORIENTED_EDGE('',*,*,#2130,.F.);
#2810=ORIENTED_EDGE('',*,*,#2131,.T.);
#2811=ORIENTED_EDGE('',*,*,#2132,.F.);
#2812=ORIENTED_EDGE('',*,*,#2131,.F.);
#2813=ORIENTED_EDGE('',*,*,#2133,.F.);
#2814=ORIENTED_EDGE('',*,*,#2125,.F.);
#2815=ORIENTED_EDGE('',*,*,#2134,.T.);
#2816=ORIENTED_EDGE('',*,*,#2126,.T.);
#2817=ORIENTED_EDGE('',*,*,#2133,.T.);
#2818=ORIENTED_EDGE('',*,*,#2130,.T.);
#2819=ORIENTED_EDGE('',*,*,#2135,.F.);
#2820=ORIENTED_EDGE('',*,*,#2127,.T.);
#2821=ORIENTED_EDGE('',*,*,#2135,.T.);
#2822=ORIENTED_EDGE('',*,*,#2129,.T.);
#2823=ORIENTED_EDGE('',*,*,#2136,.F.);
#2824=ORIENTED_EDGE('',*,*,#2117,.T.);
#2825=ORIENTED_EDGE('',*,*,#2118,.T.);
#2826=ORIENTED_EDGE('',*,*,#2137,.F.);
#2827=ORIENTED_EDGE('',*,*,#2138,.F.);
#2828=ORIENTED_EDGE('',*,*,#2139,.T.);
#2829=ORIENTED_EDGE('',*,*,#2140,.F.);
#2830=ORIENTED_EDGE('',*,*,#2139,.F.);
#2831=ORIENTED_EDGE('',*,*,#2141,.F.);
#2832=ORIENTED_EDGE('',*,*,#2142,.F.);
#2833=ORIENTED_EDGE('',*,*,#2143,.F.);
#2834=ORIENTED_EDGE('',*,*,#2144,.T.);
#2835=ORIENTED_EDGE('',*,*,#2145,.F.);
#2836=ORIENTED_EDGE('',*,*,#2144,.F.);
#2837=ORIENTED_EDGE('',*,*,#2146,.F.);
#2838=ORIENTED_EDGE('',*,*,#2147,.F.);
#2839=ORIENTED_EDGE('',*,*,#2148,.F.);
#2840=ORIENTED_EDGE('',*,*,#2149,.T.);
#2841=ORIENTED_EDGE('',*,*,#2150,.F.);
#2842=ORIENTED_EDGE('',*,*,#2149,.F.);
#2843=ORIENTED_EDGE('',*,*,#2151,.F.);
#2844=ORIENTED_EDGE('',*,*,#2152,.F.);
#2845=ORIENTED_EDGE('',*,*,#2124,.T.);
#2846=ORIENTED_EDGE('',*,*,#2136,.T.);
#2847=ORIENTED_EDGE('',*,*,#2128,.T.);
#2848=ORIENTED_EDGE('',*,*,#2132,.T.);
#2849=ORIENTED_EDGE('',*,*,#2134,.F.);
#2850=ORIENTED_EDGE('',*,*,#2153,.T.);
#2851=ORIENTED_EDGE('',*,*,#2122,.T.);
#2852=ORIENTED_EDGE('',*,*,#2121,.T.);
#2853=ORIENTED_EDGE('',*,*,#2154,.T.);
#2854=ORIENTED_EDGE('',*,*,#2152,.T.);
#2855=ORIENTED_EDGE('',*,*,#2154,.F.);
#2856=ORIENTED_EDGE('',*,*,#2120,.T.);
#2857=ORIENTED_EDGE('',*,*,#2123,.T.);
#2858=ORIENTED_EDGE('',*,*,#2153,.F.);
#2859=ORIENTED_EDGE('',*,*,#2140,.T.);
#2860=ORIENTED_EDGE('',*,*,#2145,.T.);
#2861=ORIENTED_EDGE('',*,*,#2150,.T.);
#2862=ORIENTED_EDGE('',*,*,#2155,.T.);
#2863=ORIENTED_EDGE('',*,*,#2156,.F.);
#2864=ORIENTED_EDGE('',*,*,#2141,.T.);
#2865=ORIENTED_EDGE('',*,*,#2157,.F.);
#2866=ORIENTED_EDGE('',*,*,#2146,.T.);
#2867=ORIENTED_EDGE('',*,*,#2158,.F.);
#2868=ORIENTED_EDGE('',*,*,#2151,.T.);
#2869=ORIENTED_EDGE('',*,*,#2159,.F.);
#2870=ORIENTED_EDGE('',*,*,#2155,.F.);
#2871=ORIENTED_EDGE('',*,*,#2159,.T.);
#2872=ORIENTED_EDGE('',*,*,#2148,.T.);
#2873=ORIENTED_EDGE('',*,*,#2147,.T.);
#2874=ORIENTED_EDGE('',*,*,#2158,.T.);
#2875=ORIENTED_EDGE('',*,*,#2143,.T.);
#2876=ORIENTED_EDGE('',*,*,#2142,.T.);
#2877=ORIENTED_EDGE('',*,*,#2157,.T.);
#2878=ORIENTED_EDGE('',*,*,#2138,.T.);
#2879=ORIENTED_EDGE('',*,*,#2137,.T.);
#2880=ORIENTED_EDGE('',*,*,#2156,.T.);
#2881=ORIENTED_EDGE('',*,*,#2112,.T.);
#2882=ORIENTED_EDGE('',*,*,#2113,.T.);
#2883=ORIENTED_EDGE('',*,*,#2115,.T.);
#2884=ORIENTED_EDGE('',*,*,#2116,.T.);
#3118=CYLINDRICAL_SURFACE('',#3832,0.4);
#3119=CYLINDRICAL_SURFACE('',#3833,0.25175);
#3120=CYLINDRICAL_SURFACE('',#3840,0.6);
#3121=CYLINDRICAL_SURFACE('',#3842,0.4);
#3122=CYLINDRICAL_SURFACE('',#3843,0.4);
#3123=CYLINDRICAL_SURFACE('',#3844,0.4);
#3124=CYLINDRICAL_SURFACE('',#3847,1.6);
#3262=ADVANCED_FACE('',(#645),#3118,.F.);
#3263=ADVANCED_FACE('',(#646),#3119,.F.);
#3264=ADVANCED_FACE('',(#647),#482,.F.);
#3265=ADVANCED_FACE('',(#648),#483,.F.);
#3266=ADVANCED_FACE('',(#649),#484,.F.);
#3267=ADVANCED_FACE('',(#650,#396),#485,.T.);
#3268=ADVANCED_FACE('',(#651,#397),#3120,.F.);
#3269=ADVANCED_FACE('',(#652),#3121,.T.);
#3270=ADVANCED_FACE('',(#653),#3122,.T.);
#3271=ADVANCED_FACE('',(#654),#3123,.T.);
#3272=ADVANCED_FACE('',(#655,#398),#486,.T.);
#3273=ADVANCED_FACE('',(#656,#399,#400,#401),#3124,.T.);
#3274=ADVANCED_FACE('',(#657,#402,#403),#11,.T.);
#3337=CLOSED_SHELL('',(#3262,#3263,#3264,#3265,#3266,#3267,#3268,#3269,
#3270,#3271,#3272,#3273,#3274));
#3819=AXIS2_PLACEMENT_3D('',#5952,#4611,#4612);
#3832=AXIS2_PLACEMENT_3D('',#5973,#4640,#4641);
#3833=AXIS2_PLACEMENT_3D('',#6091,#4643,#4644);
#3834=AXIS2_PLACEMENT_3D('',#6175,#4646,#4647);
#3835=AXIS2_PLACEMENT_3D('',#6184,#4652,#4653);
#3836=AXIS2_PLACEMENT_3D('',#6193,#4658,#4659);
#3837=AXIS2_PLACEMENT_3D('',#6196,#4662,#4663);
#3838=AXIS2_PLACEMENT_3D('',#6198,#4664,#4665);
#3839=AXIS2_PLACEMENT_3D('',#6199,#4666,#4667);
#3840=AXIS2_PLACEMENT_3D('',#6200,#4668,#4669);
#3841=AXIS2_PLACEMENT_3D('',#6201,#4670,#4671);
#3842=AXIS2_PLACEMENT_3D('',#6202,#4672,#4673);
#3843=AXIS2_PLACEMENT_3D('',#6292,#4675,#4676);
#3844=AXIS2_PLACEMENT_3D('',#6382,#4678,#4679);
#3845=AXIS2_PLACEMENT_3D('',#6470,#4681,#4682);
#3846=AXIS2_PLACEMENT_3D('',#6472,#4683,#4684);
#3847=AXIS2_PLACEMENT_3D('',#6473,#4685,#4686);
#3848=AXIS2_PLACEMENT_3D('',#6476,#4689,#4690);
#3849=AXIS2_PLACEMENT_3D('',#6478,#4691,#4692);
#3850=AXIS2_PLACEMENT_3D('',#6479,#4693,#4694);
#3851=AXIS2_PLACEMENT_3D('',#6480,#4695,#4696);
#3852=AXIS2_PLACEMENT_3D('',#6481,#4697,#4698);
#3853=AXIS2_PLACEMENT_3D('',#6482,#4699,#4700);
#3854=AXIS2_PLACEMENT_3D('',#6483,#4701,#4702);
#4611=DIRECTION('axis',(0.,0.,1.));
#4612=DIRECTION('refdir',(1.,0.,0.));
#4640=DIRECTION('center_axis',(0.,1.,0.));
#4641=DIRECTION('ref_axis',(1.,0.,0.));
#4642=DIRECTION('',(0.,1.,0.));
#4643=DIRECTION('center_axis',(-1.,0.,0.));
#4644=DIRECTION('ref_axis',(0.,0.,-1.));
#4645=DIRECTION('',(-1.,0.,0.));
#4646=DIRECTION('center_axis',(-1.,0.,0.));
#4647=DIRECTION('ref_axis',(0.,0.,1.));
#4648=DIRECTION('',(0.,0.,-1.));
#4649=DIRECTION('',(0.,-1.,0.));
#4650=DIRECTION('',(0.,0.,1.));
#4651=DIRECTION('',(0.,-1.,0.));
#4652=DIRECTION('center_axis',(1.,0.,0.));
#4653=DIRECTION('ref_axis',(0.,0.,-1.));
#4654=DIRECTION('',(0.,0.,1.));
#4655=DIRECTION('',(0.,1.,0.));
#4656=DIRECTION('',(0.,0.,-1.));
#4657=DIRECTION('',(0.,1.,0.));
#4658=DIRECTION('center_axis',(0.,0.,1.));
#4659=DIRECTION('ref_axis',(1.,0.,0.));
#4660=DIRECTION('',(-1.,0.,0.));
#4661=DIRECTION('',(1.,0.,0.));
#4662=DIRECTION('center_axis',(0.,-1.,0.));
#4663=DIRECTION('ref_axis',(0.,0.,-1.));
#4664=DIRECTION('center_axis',(0.,-1.,0.));
#4665=DIRECTION('ref_axis',(1.,0.,0.));
#4666=DIRECTION('center_axis',(0.,-1.,0.));
#4667=DIRECTION('ref_axis',(1.,0.,0.));
#4668=DIRECTION('center_axis',(0.,-1.,0.));
#4669=DIRECTION('ref_axis',(-1.83697019872103E-16,0.,-1.));
#4670=DIRECTION('center_axis',(0.,-1.,0.));
#4671=DIRECTION('ref_axis',(1.,0.,0.));
#4672=DIRECTION('center_axis',(-0.5,0.,0.866025403784438));
#4673=DIRECTION('ref_axis',(0.866025403784438,0.,0.5));
#4674=DIRECTION('',(0.5,0.,-0.866025403784438));
#4675=DIRECTION('center_axis',(-0.5,0.,-0.866025403784439));
#4676=DIRECTION('ref_axis',(-0.866025403784439,0.,0.5));
#4677=DIRECTION('',(0.5,0.,0.866025403784439));
#4678=DIRECTION('center_axis',(1.,0.,0.));
#4679=DIRECTION('ref_axis',(0.,0.,-1.));
#4680=DIRECTION('',(-1.,0.,0.));
#4681=DIRECTION('center_axis',(0.,1.,0.));
#4682=DIRECTION('ref_axis',(0.,0.,1.));
#4683=DIRECTION('center_axis',(0.,-1.,0.));
#4684=DIRECTION('ref_axis',(1.,0.,0.));
#4685=DIRECTION('center_axis',(0.,-1.,0.));
#4686=DIRECTION('ref_axis',(1.,0.,0.));
#4687=DIRECTION('',(0.,1.,0.));
#4688=DIRECTION('',(0.,1.,0.));
#4689=DIRECTION('center_axis',(0.,-1.,0.));
#4690=DIRECTION('ref_axis',(0.,0.,-1.));
#4691=DIRECTION('center_axis',(-1.,0.,-1.22464679914735E-16));
#4692=DIRECTION('ref_axis',(-1.22464679914735E-16,0.,1.));
#4693=DIRECTION('center_axis',(0.,1.,0.));
#4694=DIRECTION('ref_axis',(0.,0.,-1.));
#4695=DIRECTION('center_axis',(0.,1.,0.));
#4696=DIRECTION('ref_axis',(0.,0.,-1.));
#4697=DIRECTION('center_axis',(0.,1.,0.));
#4698=DIRECTION('ref_axis',(0.,0.,-1.));
#4699=DIRECTION('center_axis',(0.,1.,0.));
#4700=DIRECTION('ref_axis',(0.,0.,-1.));
#4701=DIRECTION('',(0.,0.,1.));
#4702=DIRECTION('',(1.,0.,0.));
#5952=CARTESIAN_POINT('',(0.,0.,0.));
#5973=CARTESIAN_POINT('Origin',(4.4,0.,0.));
#5974=CARTESIAN_POINT('',(4.38181818181818,-0.6,-0.399586563197017));
#5975=CARTESIAN_POINT('',(4.,-0.447213595499957,1.40845951270862E-17));
#5976=CARTESIAN_POINT('Ctrl Pts',(4.38181818181818,-0.6,-0.399586563197017));
#5977=CARTESIAN_POINT('Ctrl Pts',(4.37620354655216,-0.6,-0.399331088446446));
#5978=CARTESIAN_POINT('Ctrl Pts',(4.37059633849451,-0.599921176400794,-0.398957377684081));
#5979=CARTESIAN_POINT('Ctrl Pts',(4.35231513288062,-0.599405577873612,-0.397351597439964));
#5980=CARTESIAN_POINT('Ctrl Pts',(4.33972830709261,-0.598642847568908,-0.395635899495609));
#5981=CARTESIAN_POINT('Ctrl Pts',(4.31001303143016,-0.595878581860272,-0.390141553679429));
#5982=CARTESIAN_POINT('Ctrl Pts',(4.29310003081746,-0.593520874256089,-0.385840467860369));
#5983=CARTESIAN_POINT('Ctrl Pts',(4.24141718743348,-0.58396833212535,-0.369080440261527));
#5984=CARTESIAN_POINT('Ctrl Pts',(4.20867977226721,-0.574396002359473,-0.35308769317213));
#5985=CARTESIAN_POINT('Ctrl Pts',(4.13710416992423,-0.546662492416072,-0.305621410183058));
#5986=CARTESIAN_POINT('Ctrl Pts',(4.10145248427466,-0.526593672888128,-0.270643641048743));
#5987=CARTESIAN_POINT('Ctrl Pts',(4.04678809651788,-0.489398581579535,-0.193271805068502));
#5988=CARTESIAN_POINT('Ctrl Pts',(4.02636517822878,-0.471824419974506,-0.150618280859474));
#5989=CARTESIAN_POINT('Ctrl Pts',(4.00475562957405,-0.45203353900844,-0.0707222616040669));
#5990=CARTESIAN_POINT('Ctrl Pts',(4.,-0.447213595499957,-0.0358213625930324));
#5991=CARTESIAN_POINT('Ctrl Pts',(4.,-0.447213595499957,0.));
#5992=CARTESIAN_POINT('Ctrl Pts',(4.,-0.447213595499957,-4.2096619668615E-17));
#5993=CARTESIAN_POINT('Ctrl Pts',(4.,-0.447213595499957,0.00231828024966431));
#5994=CARTESIAN_POINT('Ctrl Pts',(4.00002015291119,-0.447233426516538,0.00464041591900193));
#5995=CARTESIAN_POINT('Ctrl Pts',(4.00078593665181,-0.447986619321796,0.0486042900487314));
#5996=CARTESIAN_POINT('Ctrl Pts',(4.00791128215643,-0.455206051708779,0.0886447085746181));
#5997=CARTESIAN_POINT('Ctrl Pts',(4.03587474981726,-0.479963706911242,0.172535559232532));
#5998=CARTESIAN_POINT('Ctrl Pts',(4.05952154543374,-0.499305325617665,0.215544140194275));
#5999=CARTESIAN_POINT('Ctrl Pts',(4.115931958945,-0.534538341716186,0.284471526737177));
#6000=CARTESIAN_POINT('Ctrl Pts',(4.14628233661512,-0.550362037136641,0.311973849714753));
#6001=CARTESIAN_POINT('Ctrl Pts',(4.21006393264307,-0.574803374422168,0.353766344633894));
#6002=CARTESIAN_POINT('Ctrl Pts',(4.24216830962295,-0.584104086647922,0.369319268652553));
#6003=CARTESIAN_POINT('Ctrl Pts',(4.29308262177289,-0.59351913040989,0.385837098757871));
#6004=CARTESIAN_POINT('Ctrl Pts',(4.31000257334402,-0.595876699074913,0.390138254734081));
#6005=CARTESIAN_POINT('Ctrl Pts',(4.33984346373323,-0.59865422370305,0.395658187711044));
#6006=CARTESIAN_POINT('Ctrl Pts',(4.35255940167626,-0.59942003186583,0.397384387659598));
#6007=CARTESIAN_POINT('Ctrl Pts',(4.37864659775072,-0.600140148714188,0.399652395423929));
#6008=CARTESIAN_POINT('Ctrl Pts',(4.39197122976054,-0.600060372790861,0.400141070011449));
#6009=CARTESIAN_POINT('Ctrl Pts',(4.42524642236728,-0.598768169203699,0.399701228150437));
#6010=CARTESIAN_POINT('Ctrl Pts',(4.44505102882446,-0.597014891071304,0.397946347201428));
#6011=CARTESIAN_POINT('Ctrl Pts',(4.51231374643158,-0.587907156256967,0.386945439318973));
#6012=CARTESIAN_POINT('Ctrl Pts',(4.55722896459207,-0.576234031361068,0.370738351126727));
#6013=CARTESIAN_POINT('Ctrl Pts',(4.64383263048066,-0.5452156510398,0.321498513032364));
#6014=CARTESIAN_POINT('Ctrl Pts',(4.68382910146734,-0.525117270017781,0.286611708354837));
#6015=CARTESIAN_POINT('Ctrl Pts',(4.74479838771145,-0.488962051837591,0.208211119095925));
#6016=CARTESIAN_POINT('Ctrl Pts',(4.76751221814709,-0.472539690182888,0.16532363822899));
#6017=CARTESIAN_POINT('Ctrl Pts',(4.793947837701,-0.45233115292012,0.0801450491942168));
#6018=CARTESIAN_POINT('Ctrl Pts',(4.80013660259258,-0.447101597189361,0.0399141590418927));
#6019=CARTESIAN_POINT('Ctrl Pts',(4.79985042703662,-0.447336228030294,-0.0451141645597526));
#6020=CARTESIAN_POINT('Ctrl Pts',(4.79259442840285,-0.453470503705387,-0.0875565986513605));
#6021=CARTESIAN_POINT('Ctrl Pts',(4.76254336881826,-0.476181588957065,-0.176742802554312));
#6022=CARTESIAN_POINT('Ctrl Pts',(4.73698137926376,-0.494272007313214,-0.221226370718438));
#6023=CARTESIAN_POINT('Ctrl Pts',(4.67589300813802,-0.528959279983926,-0.292989120825645));
#6024=CARTESIAN_POINT('Ctrl Pts',(4.64156068949428,-0.545654377209448,-0.321979194943134));
#6025=CARTESIAN_POINT('Ctrl Pts',(4.57349950221702,-0.570649410723138,-0.362013117337885));
#6026=CARTESIAN_POINT('Ctrl Pts',(4.54174415913774,-0.579993920599389,-0.375669546647045));
#6027=CARTESIAN_POINT('Ctrl Pts',(4.48184469738762,-0.59235489505887,-0.392487976854985));
#6028=CARTESIAN_POINT('Ctrl Pts',(4.45469661582122,-0.596251830509523,-0.397210764878501));
#6029=CARTESIAN_POINT('Ctrl Pts',(4.41199868606709,-0.599430494173245,-0.400104322948797));
#6030=CARTESIAN_POINT('Ctrl Pts',(4.3969025511922,-0.6,-0.40027292576925));
#6031=CARTESIAN_POINT('Ctrl Pts',(4.38181818181818,-0.6,-0.399586563197017));
#6032=CARTESIAN_POINT('',(4.,0.447213595499957,1.06151481751326E-17));
#6033=CARTESIAN_POINT('',(4.,0.,4.89858719658942E-17));
#6034=CARTESIAN_POINT('',(4.38181818181818,0.6,-0.399586563197017));
#6035=CARTESIAN_POINT('Ctrl Pts',(4.38181818181818,0.6,-0.399586563197017));
#6036=CARTESIAN_POINT('Ctrl Pts',(4.38217776987594,0.6,-0.399602925020183));
#6037=CARTESIAN_POINT('Ctrl Pts',(4.38253737948503,0.599999676740854,-0.399618801429084));
#6038=CARTESIAN_POINT('Ctrl Pts',(4.39810750269961,0.599971691179406,-0.400285149978334));
#6039=CARTESIAN_POINT('Ctrl Pts',(4.41335962542107,0.599365583135745,-0.400068337184671));
#6040=CARTESIAN_POINT('Ctrl Pts',(4.45609605239849,0.596076444344949,-0.39700592354558));
#6041=CARTESIAN_POINT('Ctrl Pts',(4.48315173565338,0.59213819454422,-0.392211691390051));
#6042=CARTESIAN_POINT('Ctrl Pts',(4.5562274106725,0.576906850691916,-0.371434861078584));
#6043=CARTESIAN_POINT('Ctrl Pts',(4.5994416592477,0.562448501081322,-0.349930526910355));
#6044=CARTESIAN_POINT('Ctrl Pts',(4.68197093066801,0.526887929791366,-0.289059421938731));
#6045=CARTESIAN_POINT('Ctrl Pts',(4.71927072326363,0.505032168549575,-0.247311177133964));
#6046=CARTESIAN_POINT('Ctrl Pts',(4.76835617637136,0.472224573632385,-0.161747869091691));
#6047=CARTESIAN_POINT('Ctrl Pts',(4.78412913104805,0.459943187027168,-0.120335510170092));
#6048=CARTESIAN_POINT('Ctrl Pts',(4.8004842088633,0.446911473500065,-0.0358681413616309));
#6049=CARTESIAN_POINT('Ctrl Pts',(4.80211129711387,0.445512317526093,0.00512209912648909));
#6050=CARTESIAN_POINT('Ctrl Pts',(4.79189040150874,0.45380427042988,0.0928053928501807));
#6051=CARTESIAN_POINT('Ctrl Pts',(4.77850571140352,0.464665209937273,0.136981831350341));
#6052=CARTESIAN_POINT('Ctrl Pts',(4.73651199214904,0.493999272271238,0.221864434033125));
#6053=CARTESIAN_POINT('Ctrl Pts',(4.70652254298001,0.512942829957004,0.261673250221586));
#6054=CARTESIAN_POINT('Ctrl Pts',(4.63981283945647,0.545961862488824,0.322778046340775));
#6055=CARTESIAN_POINT('Ctrl Pts',(4.60484752125829,0.560431345960551,0.346187806499183));
#6056=CARTESIAN_POINT('Ctrl Pts',(4.53107703569756,0.58280302533232,0.379877153356344));
#6057=CARTESIAN_POINT('Ctrl Pts',(4.49327004619306,0.591089762190358,0.391021773957148));
#6058=CARTESIAN_POINT('Ctrl Pts',(4.43565722321789,0.597872083748138,0.3988217367562));
#6059=CARTESIAN_POINT('Ctrl Pts',(4.41740282127395,0.599230533101231,0.400044418723135));
#6060=CARTESIAN_POINT('Ctrl Pts',(4.38605291211989,0.600123801224883,0.399966620420395));
#6061=CARTESIAN_POINT('Ctrl Pts',(4.37307485581441,0.600078055860439,0.399305346447973));
#6062=CARTESIAN_POINT('Ctrl Pts',(4.34707983335796,0.599129994834138,0.396700137951532));
#6063=CARTESIAN_POINT('Ctrl Pts',(4.3341144934305,0.598224910034854,0.394754522931063));
#6064=CARTESIAN_POINT('Ctrl Pts',(4.30271417169121,0.594971578276487,0.388449597781707));
#6065=CARTESIAN_POINT('Ctrl Pts',(4.28453727637576,0.592176175294015,0.383433197654118));
#6066=CARTESIAN_POINT('Ctrl Pts',(4.22586458639984,0.580243538593361,0.362717744715626));
#6067=CARTESIAN_POINT('Ctrl Pts',(4.18833529340542,0.567737042053699,0.341993684570505));
#6068=CARTESIAN_POINT('Ctrl Pts',(4.11283462612631,0.534171378857267,0.283547383735074));
#6069=CARTESIAN_POINT('Ctrl Pts',(4.07888753653551,0.51231402191844,0.243724831889356));
#6070=CARTESIAN_POINT('Ctrl Pts',(4.03269086728519,0.477679254985282,0.16387858814032));
#6071=CARTESIAN_POINT('Ctrl Pts',(4.01686967046718,0.463294474516269,0.123253857821745));
#6072=CARTESIAN_POINT('Ctrl Pts',(4.00269233005712,0.449913571793227,0.0534756547949087));
#6073=CARTESIAN_POINT('Ctrl Pts',(4.,0.447213595499957,0.0269126210022609));
#6074=CARTESIAN_POINT('Ctrl Pts',(4.,0.447213595499957,-2.77555756156289E-17));
#6075=CARTESIAN_POINT('Ctrl Pts',(4.,0.447213595499957,3.12250225675825E-17));
#6076=CARTESIAN_POINT('Ctrl Pts',(4.,0.447213595499957,-0.0109336371758505));
#6077=CARTESIAN_POINT('Ctrl Pts',(4.00044757096773,0.447655562220312,-0.0219249776368444));
#6078=CARTESIAN_POINT('Ctrl Pts',(4.00520900670299,0.452307037407336,-0.0794936286785903));
#6079=CARTESIAN_POINT('Ctrl Pts',(4.01683899054454,0.463589521272128,-0.121314660456946));
#6080=CARTESIAN_POINT('Ctrl Pts',(4.05044411504352,0.491640345747449,-0.199899424965473));
#6081=CARTESIAN_POINT('Ctrl Pts',(4.07632395532653,0.511152433757493,-0.239920550986411));
#6082=CARTESIAN_POINT('Ctrl Pts',(4.14319162351432,0.549072366528989,-0.310568720434486));
#6083=CARTESIAN_POINT('Ctrl Pts',(4.18393657245712,0.567086215733065,-0.340536354364695));
#6084=CARTESIAN_POINT('Ctrl Pts',(4.25308519475938,0.586109821373136,-0.372873616714749));
#6085=CARTESIAN_POINT('Ctrl Pts',(4.27683034868435,0.591075841926799,-0.381421283524454));
#6086=CARTESIAN_POINT('Ctrl Pts',(4.31562065419949,0.596457618518653,-0.391266435776889));
#6087=CARTESIAN_POINT('Ctrl Pts',(4.32991058664294,0.597905515290278,-0.394084038616911));
#6088=CARTESIAN_POINT('Ctrl Pts',(4.35677956565808,0.599605121795544,-0.397853848713028));
#6089=CARTESIAN_POINT('Ctrl Pts',(4.36925538216825,0.6,-0.399014936020011));
#6090=CARTESIAN_POINT('Ctrl Pts',(4.38181818181818,0.6,-0.399586563197017));
#6091=CARTESIAN_POINT('Origin',(-0.5,0.,0.));
#6092=CARTESIAN_POINT('',(-0.544630092356271,-2.77555756156289E-17,-0.25175));
#6093=CARTESIAN_POINT('',(-0.544630092356271,3.08304831685346E-17,0.25175));
#6094=CARTESIAN_POINT('Ctrl Pts',(-0.544630092356271,-2.77555756156289E-17,
-0.25175));
#6095=CARTESIAN_POINT('Ctrl Pts',(-0.544630092356271,-0.0320661161546808,
-0.25175));
#6096=CARTESIAN_POINT('Ctrl Pts',(-0.547762140631641,-0.0659494177282828,
-0.245259980626381));
#6097=CARTESIAN_POINT('Ctrl Pts',(-0.558600363408959,-0.127829426180881,
-0.219457148015658));
#6098=CARTESIAN_POINT('Ctrl Pts',(-0.566103947925634,-0.155868059910982,
-0.200160204416444));
#6099=CARTESIAN_POINT('Ctrl Pts',(-0.579856011772299,-0.200132614131413,
-0.155895650196014));
#6100=CARTESIAN_POINT('Ctrl Pts',(-0.587059973454843,-0.219450369823919,
-0.127846763396003));
#6101=CARTESIAN_POINT('Ctrl Pts',(-0.597191733030102,-0.245269281484808,
-0.0659260305857526));
#6102=CARTESIAN_POINT('Ctrl Pts',(-0.6,-0.25175,-0.0320261671617185));
#6103=CARTESIAN_POINT('Ctrl Pts',(-0.6,-0.25175,0.0320261671617186));
#6104=CARTESIAN_POINT('Ctrl Pts',(-0.597191733030102,-0.245269281484808,
0.0659260305857528));
#6105=CARTESIAN_POINT('Ctrl Pts',(-0.587059973454843,-0.219450369823919,
0.127846763396003));
#6106=CARTESIAN_POINT('Ctrl Pts',(-0.579856011772299,-0.200132614131413,
0.155895650196014));
#6107=CARTESIAN_POINT('Ctrl Pts',(-0.566103947925634,-0.155868059910982,
0.200160204416444));
#6108=CARTESIAN_POINT('Ctrl Pts',(-0.558600363408959,-0.127829426180881,
0.219457148015658));
#6109=CARTESIAN_POINT('Ctrl Pts',(-0.547762140631641,-0.0659494177282828,
0.245259980626381));
#6110=CARTESIAN_POINT('Ctrl Pts',(-0.544630092356271,-0.0320661161546807,
0.25175));
#6111=CARTESIAN_POINT('Ctrl Pts',(-0.544630092356271,0.,0.25175));
#6112=CARTESIAN_POINT('Ctrl Pts',(-0.544630092356271,2.08166817117217E-17,
0.25175));
#6113=CARTESIAN_POINT('Ctrl Pts',(-0.544630092356271,0.0320661161546808,
0.25175));
#6114=CARTESIAN_POINT('Ctrl Pts',(-0.547762140631641,0.0659494177282828,
0.245259980626381));
#6115=CARTESIAN_POINT('Ctrl Pts',(-0.558600363408959,0.127829426180881,
0.219457148015658));
#6116=CARTESIAN_POINT('Ctrl Pts',(-0.566103947925634,0.155868059910982,
0.200160204416444));
#6117=CARTESIAN_POINT('Ctrl Pts',(-0.579856011772299,0.200132614131413,
0.155895650196014));
#6118=CARTESIAN_POINT('Ctrl Pts',(-0.587059973454843,0.219450369823919,
0.127846763396003));
#6119=CARTESIAN_POINT('Ctrl Pts',(-0.597191733030102,0.245269281484808,
0.0659260305857527));
#6120=CARTESIAN_POINT('Ctrl Pts',(-0.6,0.25175,0.0320261671617186));
#6121=CARTESIAN_POINT('Ctrl Pts',(-0.6,0.25175,-0.0320261671617186));
#6122=CARTESIAN_POINT('Ctrl Pts',(-0.597191733030102,0.245269281484808,
-0.0659260305857527));
#6123=CARTESIAN_POINT('Ctrl Pts',(-0.587059973454843,0.219450369823919,
-0.127846763396003));
#6124=CARTESIAN_POINT('Ctrl Pts',(-0.579856011772299,0.200132614131413,
-0.155895650196014));
#6125=CARTESIAN_POINT('Ctrl Pts',(-0.566103947925634,0.155868059910982,
-0.200160204416444));
#6126=CARTESIAN_POINT('Ctrl Pts',(-0.558600363408959,0.127829426180881,
-0.219457148015658));
#6127=CARTESIAN_POINT('Ctrl Pts',(-0.547762140631641,0.0659494177282829,
-0.245259980626381));
#6128=CARTESIAN_POINT('Ctrl Pts',(-0.544630092356271,0.0320661161546808,
-0.25175));
#6129=CARTESIAN_POINT('Ctrl Pts',(-0.544630092356271,1.38777878078145E-17,
-0.25175));
#6130=CARTESIAN_POINT('',(-1.58007023182516,1.88846885362209E-17,0.25175));
#6131=CARTESIAN_POINT('',(-0.5,3.08304831685346E-17,0.25175));
#6132=CARTESIAN_POINT('',(-1.6,0.25175,-8.06245091720202E-17));
#6133=CARTESIAN_POINT('Ctrl Pts',(-1.6,0.25175,3.46944695195361E-17));
#6134=CARTESIAN_POINT('Ctrl Pts',(-1.6,0.25175,0.0316665562812107));
#6135=CARTESIAN_POINT('Ctrl Pts',(-1.59896422950043,0.245410672078977,0.0654081672606842));
#6136=CARTESIAN_POINT('Ctrl Pts',(-1.59522075716076,0.219702194881036,0.127418882159871));
#6137=CARTESIAN_POINT('Ctrl Pts',(-1.59256535387617,0.200335934524935,0.155692329802492));
#6138=CARTESIAN_POINT('Ctrl Pts',(-1.58756727523672,0.155691857576545,0.200336406750882));
#6139=CARTESIAN_POINT('Ctrl Pts',(-1.58489737644125,0.12741861324567,0.219702296671568));
#6140=CARTESIAN_POINT('Ctrl Pts',(-1.58112064026101,0.0654085945942507,
0.245410504610724));
#6141=CARTESIAN_POINT('Ctrl Pts',(-1.58007023182516,0.0316672261988669,
0.25175));
#6142=CARTESIAN_POINT('Ctrl Pts',(-1.58007023182516,-6.93889390390723E-18,
0.25175));
#6143=CARTESIAN_POINT('',(-1.58007023182516,0.,-0.25175));
#6144=CARTESIAN_POINT('Ctrl Pts',(-1.58007023182516,0.,-0.25175));
#6145=CARTESIAN_POINT('Ctrl Pts',(-1.58007023182516,0.0316672261988669,
-0.25175));
#6146=CARTESIAN_POINT('Ctrl Pts',(-1.58112064026101,0.0654085945942508,
-0.245410504610724));
#6147=CARTESIAN_POINT('Ctrl Pts',(-1.58489737644125,0.12741861324567,-0.219702296671568));
#6148=CARTESIAN_POINT('Ctrl Pts',(-1.58756727523672,0.155691857576545,-0.200336406750882));
#6149=CARTESIAN_POINT('Ctrl Pts',(-1.59256535387617,0.200335934524935,-0.155692329802492));
#6150=CARTESIAN_POINT('Ctrl Pts',(-1.59522075716076,0.219702194881036,-0.127418882159871));
#6151=CARTESIAN_POINT('Ctrl Pts',(-1.59896422950043,0.245410672078977,-0.0654081672606842));
#6152=CARTESIAN_POINT('Ctrl Pts',(-1.6,0.25175,-0.0316665562812106));
#6153=CARTESIAN_POINT('Ctrl Pts',(-1.6,0.25175,4.16333634234434E-17));
#6154=CARTESIAN_POINT('',(-1.6,-0.25175,-1.01441190883742E-16));
#6155=CARTESIAN_POINT('Ctrl Pts',(-1.6,-0.25175,-6.93889390390723E-18));
#6156=CARTESIAN_POINT('Ctrl Pts',(-1.6,-0.25175,-0.0316665562812106));
#6157=CARTESIAN_POINT('Ctrl Pts',(-1.59896422950043,-0.245410672078977,
-0.0654081672606842));
#6158=CARTESIAN_POINT('Ctrl Pts',(-1.59522075716076,-0.219702194881036,
-0.127418882159871));
#6159=CARTESIAN_POINT('Ctrl Pts',(-1.59256535387617,-0.200335934524935,
-0.155692329802492));
#6160=CARTESIAN_POINT('Ctrl Pts',(-1.58756727523672,-0.155691857576545,
-0.200336406750882));
#6161=CARTESIAN_POINT('Ctrl Pts',(-1.58489737644125,-0.12741861324567,-0.219702296671568));
#6162=CARTESIAN_POINT('Ctrl Pts',(-1.58112064026101,-0.0654085945942508,
-0.245410504610724));
#6163=CARTESIAN_POINT('Ctrl Pts',(-1.58007023182516,-0.0316672261988669,
-0.25175));
#6164=CARTESIAN_POINT('Ctrl Pts',(-1.58007023182516,0.,-0.25175));
#6165=CARTESIAN_POINT('Ctrl Pts',(-1.58007023182516,-6.93889390390723E-18,
0.25175));
#6166=CARTESIAN_POINT('Ctrl Pts',(-1.58007023182516,-0.0316672261988669,
0.25175));
#6167=CARTESIAN_POINT('Ctrl Pts',(-1.58112064026101,-0.0654085945942507,
0.245410504610724));
#6168=CARTESIAN_POINT('Ctrl Pts',(-1.58489737644125,-0.12741861324567,0.219702296671568));
#6169=CARTESIAN_POINT('Ctrl Pts',(-1.58756727523672,-0.155691857576545,
0.200336406750882));
#6170=CARTESIAN_POINT('Ctrl Pts',(-1.59256535387617,-0.200335934524935,
0.155692329802492));
#6171=CARTESIAN_POINT('Ctrl Pts',(-1.59522075716076,-0.219702194881036,
0.127418882159871));
#6172=CARTESIAN_POINT('Ctrl Pts',(-1.59896422950043,-0.245410672078977,
0.0654081672606843));
#6173=CARTESIAN_POINT('Ctrl Pts',(-1.6,-0.25175,0.0316665562812106));
#6174=CARTESIAN_POINT('Ctrl Pts',(-1.6,-0.25175,0.));
#6175=CARTESIAN_POINT('Origin',(-0.2,0.,0.55));
#6176=CARTESIAN_POINT('',(-0.2,1.9,0.78));
#6177=CARTESIAN_POINT('',(-0.2,1.9,0.565685424949238));
#6178=CARTESIAN_POINT('',(-0.2,1.9,0.275));
#6179=CARTESIAN_POINT('',(-0.2,-1.9,0.78));
#6180=CARTESIAN_POINT('',(-0.2,0.,0.78));
#6181=CARTESIAN_POINT('',(-0.2,-1.9,0.565685424949238));
#6182=CARTESIAN_POINT('',(-0.2,-1.9,0.275));
#6183=CARTESIAN_POINT('',(-0.2,0.,0.565685424949238));
#6184=CARTESIAN_POINT('Origin',(0.2,0.,0.78));
#6185=CARTESIAN_POINT('',(0.2,1.9,0.565685424949238));
#6186=CARTESIAN_POINT('',(0.2,1.9,0.78));
#6187=CARTESIAN_POINT('',(0.2,1.9,0.39));
#6188=CARTESIAN_POINT('',(0.2,-1.9,0.565685424949238));
#6189=CARTESIAN_POINT('',(0.2,0.,0.565685424949238));
#6190=CARTESIAN_POINT('',(0.2,-1.9,0.78));
#6191=CARTESIAN_POINT('',(0.2,-1.9,0.39));
#6192=CARTESIAN_POINT('',(0.2,0.,0.78));
#6193=CARTESIAN_POINT('Origin',(-0.2,0.,0.78));
#6194=CARTESIAN_POINT('',(0.7,1.9,0.78));
#6195=CARTESIAN_POINT('',(0.2,-1.9,0.78));
#6196=CARTESIAN_POINT('Origin',(0.6,-1.9,0.));
#6197=CARTESIAN_POINT('',(-1.6,-1.9,-1.95943487863577E-16));
#6198=CARTESIAN_POINT('Origin',(0.,-1.9,0.));
#6199=CARTESIAN_POINT('Origin',(0.,-1.9,0.));
#6200=CARTESIAN_POINT('Origin',(0.,0.,0.));
#6201=CARTESIAN_POINT('Origin',(0.,1.9,0.));
#6202=CARTESIAN_POINT('Origin',(-0.700000000000001,0.,1.21243556529821));
#6203=CARTESIAN_POINT('',(-1.97639320225002,-0.4,3.42321344203079));
#6204=CARTESIAN_POINT('',(-1.54303420125535,4.36782978783278E-17,3.47261363439071));
#6205=CARTESIAN_POINT('Ctrl Pts',(-1.97639320225002,-0.4,3.42321344203079));
#6206=CARTESIAN_POINT('Ctrl Pts',(-1.95415831773611,-0.4,3.4360507585903));
#6207=CARTESIAN_POINT('Ctrl Pts',(-1.9310257528573,-0.397543666260907,3.44654300794432));
#6208=CARTESIAN_POINT('Ctrl Pts',(-1.87011275937252,-0.385296442875872,
3.46805551377425));
#6209=CARTESIAN_POINT('Ctrl Pts',(-1.83255059885217,-0.372362902338019,
3.47567016958921));
#6210=CARTESIAN_POINT('Ctrl Pts',(-1.74343033527116,-0.329622538051278,
3.48635323641216));
#6211=CARTESIAN_POINT('Ctrl Pts',(-1.69170226994963,-0.293529822220925,
3.48570386152998));
#6212=CARTESIAN_POINT('Ctrl Pts',(-1.61564653912222,-0.213132057516649,
3.4812739628721));
#6213=CARTESIAN_POINT('Ctrl Pts',(-1.58806423417247,-0.172744633626715,
3.4782529204836));
#6214=CARTESIAN_POINT('Ctrl Pts',(-1.55315160595641,-0.0896107157758499,
3.47405876016096));
#6215=CARTESIAN_POINT('Ctrl Pts',(-1.5440326911925,-0.048847909102319,3.47275072127476));
#6216=CARTESIAN_POINT('Ctrl Pts',(-1.54305991676911,-0.00467961343368063,
3.47261716680632));
#6217=CARTESIAN_POINT('Ctrl Pts',(-1.54303420125535,-0.00233835250145938,
3.47261363439071));
#6218=CARTESIAN_POINT('Ctrl Pts',(-1.54303420125535,1.04859257011983E-17,
3.47261363439071));
#6219=CARTESIAN_POINT('',(-2.2358545242829,-2.10234890309935E-17,3.07261363439071));
#6220=CARTESIAN_POINT('Ctrl Pts',(-2.2358545242829,-2.08166817117217E-17,
3.07261363439071));
#6221=CARTESIAN_POINT('Ctrl Pts',(-2.2358545242829,-0.0383517947844003,
3.07261363439071));
#6222=CARTESIAN_POINT('Ctrl Pts',(-2.23325695879738,-0.0760113765503611,
3.0790942798427));
#6223=CARTESIAN_POINT('Ctrl Pts',(-2.22115055352356,-0.160957090841631,
3.10774035695596));
#6224=CARTESIAN_POINT('Ctrl Pts',(-2.20980404970244,-0.205137357634188,
3.134001114773));
#6225=CARTESIAN_POINT('Ctrl Pts',(-2.17521580468705,-0.28961400567012,3.20357758115091));
#6226=CARTESIAN_POINT('Ctrl Pts',(-2.15015969108582,-0.326524134432438,
3.24882900544019));
#6227=CARTESIAN_POINT('Ctrl Pts',(-2.09653256150325,-0.370775784308148,
3.32158936294835));
#6228=CARTESIAN_POINT('Ctrl Pts',(-2.07090576981203,-0.384320524321436,
3.35106094569693));
#6229=CARTESIAN_POINT('Ctrl Pts',(-2.02085331447703,-0.397355586307629,
3.39445851101291));
#6230=CARTESIAN_POINT('Ctrl Pts',(-1.99946741642565,-0.4,3.40989153826515));
#6231=CARTESIAN_POINT('Ctrl Pts',(-1.97639320225002,-0.4,3.42321344203079));
#6232=CARTESIAN_POINT('',(-1.12100683075526,0.,1.14164078649987));
#6233=CARTESIAN_POINT('',(-1.04641016151378,-4.89858719658941E-17,1.01243556529821));
#6234=CARTESIAN_POINT('Ctrl Pts',(-1.12100683075526,0.,1.14164078649987));
#6235=CARTESIAN_POINT('Ctrl Pts',(-1.12100683075526,0.0504597642713565,
1.14164078649987));
#6236=CARTESIAN_POINT('Ctrl Pts',(-1.11359645548276,0.1041286832042,1.1490623967528));
#6237=CARTESIAN_POINT('Ctrl Pts',(-1.08303934555689,0.202612274012173,1.17790798500778));
#6238=CARTESIAN_POINT('Ctrl Pts',(-1.05982504365452,0.247446581818911,1.19919313648287));
#6239=CARTESIAN_POINT('Ctrl Pts',(-1.00487832123842,0.318233894120626,1.24559724615223));
#6240=CARTESIAN_POINT('Ctrl Pts',(-0.969414884906718,0.348984503722909,
1.27384551059033));
#6241=CARTESIAN_POINT('Ctrl Pts',(-0.888861576521062,0.389873348412022,
1.33130488677705));
#6242=CARTESIAN_POINT('Ctrl Pts',(-0.843693327768004,0.4,1.36041429150645));
#6243=CARTESIAN_POINT('Ctrl Pts',(-0.756306672231997,0.4,1.41086700060375));
#6244=CARTESIAN_POINT('Ctrl Pts',(-0.708513063870764,0.389873348412022,
1.43542914910365));
#6245=CARTESIAN_POINT('Ctrl Pts',(-0.618475130214631,0.348984503722909,
1.47646067243115));
#6246=CARTESIAN_POINT('Ctrl Pts',(-0.576279697432564,0.318233894120626,
1.49304877698084));
#6247=CARTESIAN_POINT('Ctrl Pts',(-0.508619198410849,0.247446581818911,
1.5174319796132));
#6248=CARTESIAN_POINT('Ctrl Pts',(-0.478578565558828,0.202612274012173,
1.52689357905423));
#6249=CARTESIAN_POINT('Ctrl Pts',(-0.438318998379975,0.1041286832042,1.53893401838878));
#6250=CARTESIAN_POINT('Ctrl Pts',(-0.428186507727709,0.0504597642713565,
1.54164078649987));
#6251=CARTESIAN_POINT('Ctrl Pts',(-0.428186507727709,-0.0504597642713564,
1.54164078649987));
#6252=CARTESIAN_POINT('Ctrl Pts',(-0.438318998379975,-0.1041286832042,1.53893401838878));
#6253=CARTESIAN_POINT('Ctrl Pts',(-0.478578565558828,-0.202612274012173,
1.52689357905423));
#6254=CARTESIAN_POINT('Ctrl Pts',(-0.508619198410849,-0.247446581818911,
1.5174319796132));
#6255=CARTESIAN_POINT('Ctrl Pts',(-0.576279697432564,-0.318233894120626,
1.49304877698084));
#6256=CARTESIAN_POINT('Ctrl Pts',(-0.618475130214631,-0.348984503722909,
1.47646067243115));
#6257=CARTESIAN_POINT('Ctrl Pts',(-0.708513063870764,-0.389873348412022,
1.43542914910365));
#6258=CARTESIAN_POINT('Ctrl Pts',(-0.756306672231997,-0.4,1.41086700060375));
#6259=CARTESIAN_POINT('Ctrl Pts',(-0.843693327768004,-0.4,1.36041429150645));
#6260=CARTESIAN_POINT('Ctrl Pts',(-0.888861576521062,-0.389873348412022,
1.33130488677705));
#6261=CARTESIAN_POINT('Ctrl Pts',(-0.969414884906718,-0.348984503722909,
1.27384551059033));
#6262=CARTESIAN_POINT('Ctrl Pts',(-1.00487832123842,-0.318233894120626,
1.24559724615223));
#6263=CARTESIAN_POINT('Ctrl Pts',(-1.05982504365452,-0.247446581818911,
1.19919313648287));
#6264=CARTESIAN_POINT('Ctrl Pts',(-1.08303934555689,-0.202612274012173,
1.17790798500778));
#6265=CARTESIAN_POINT('Ctrl Pts',(-1.11359645548276,-0.1041286832042,1.1490623967528));
#6266=CARTESIAN_POINT('Ctrl Pts',(-1.12100683075526,-0.0504597642713565,
1.14164078649987));
#6267=CARTESIAN_POINT('Ctrl Pts',(-1.12100683075526,-1.38777878078145E-17,
1.14164078649987));
#6268=CARTESIAN_POINT('Ctrl Pts',(-1.54303420125535,6.24500451351651E-17,
3.47261363439071));
#6269=CARTESIAN_POINT('Ctrl Pts',(-1.54303420125535,0.0410730673371918,
3.47261363439071));
#6270=CARTESIAN_POINT('Ctrl Pts',(-1.55095885731966,0.0812488103419988,
3.47375555118006));
#6271=CARTESIAN_POINT('Ctrl Pts',(-1.58495764629444,0.168643605332508,3.47792115802208));
#6272=CARTESIAN_POINT('Ctrl Pts',(-1.61486601851427,0.212871126833583,3.48130423813646));
#6273=CARTESIAN_POINT('Ctrl Pts',(-1.68826827178664,0.289288653612537,3.48542183788627));
#6274=CARTESIAN_POINT('Ctrl Pts',(-1.73220819761744,0.321562705912147,3.4861545786764));
#6275=CARTESIAN_POINT('Ctrl Pts',(-1.81695233056502,0.366289871498909,3.47834349980413));
#6276=CARTESIAN_POINT('Ctrl Pts',(-1.8573504302408,0.38158281389927,3.47138302834526));
#6277=CARTESIAN_POINT('Ctrl Pts',(-1.92264474793187,0.396376989861723,3.45003490626818));
#6278=CARTESIAN_POINT('Ctrl Pts',(-1.94731404531759,0.399534030132352,3.43946670387874));
#6279=CARTESIAN_POINT('Ctrl Pts',(-1.99398984114484,0.400357587283029,3.4134650277082));
#6280=CARTESIAN_POINT('Ctrl Pts',(-2.01531311918225,0.398184081632147,3.3986128265759));
#6281=CARTESIAN_POINT('Ctrl Pts',(-2.06441253258454,0.386733579315055,3.35745440071872));
#6282=CARTESIAN_POINT('Ctrl Pts',(-2.08944120109624,0.37471741504947,3.32984347089212));
#6283=CARTESIAN_POINT('Ctrl Pts',(-2.1435825547406,0.334141370748261,3.25932472726254));
#6284=CARTESIAN_POINT('Ctrl Pts',(-2.16934579305907,0.299193471253548,3.21427723761843));
#6285=CARTESIAN_POINT('Ctrl Pts',(-2.20475499729868,0.22024819873023,3.14480978899578));
#6286=CARTESIAN_POINT('Ctrl Pts',(-2.21652694497689,0.17986122270608,3.11828750797817));
#6287=CARTESIAN_POINT('Ctrl Pts',(-2.23122850773119,0.0967734525439114,
3.08409367525424));
#6288=CARTESIAN_POINT('Ctrl Pts',(-2.23502289292351,0.0560978356893851,
3.07465248016042));
#6289=CARTESIAN_POINT('Ctrl Pts',(-2.23581459500602,0.00945212461835248,
3.07271160407144));
#6290=CARTESIAN_POINT('Ctrl Pts',(-2.2358545242829,0.00472081811281322,
3.07261363439071));
#6291=CARTESIAN_POINT('Ctrl Pts',(-2.2358545242829,-6.29346629103429E-18,
3.07261363439071));
#6292=CARTESIAN_POINT('Origin',(-0.7,0.,-1.21243556529821));
#6293=CARTESIAN_POINT('',(-1.97639320225002,-0.4,-3.42321344203079));
#6294=CARTESIAN_POINT('',(-2.23585452428289,1.93921692146525E-17,-3.07261363439072));
#6295=CARTESIAN_POINT('Ctrl Pts',(-1.97639320225002,-0.4,-3.42321344203079));
#6296=CARTESIAN_POINT('Ctrl Pts',(-1.99862808676393,-0.4,-3.41037612547128));
#6297=CARTESIAN_POINT('Ctrl Pts',(-2.01928092368676,-0.397543666260908,
-3.39558886130855));
#6298=CARTESIAN_POINT('Ctrl Pts',(-2.06836779697694,-0.385296442875871,
-3.35359291444514));
#6299=CARTESIAN_POINT('Ctrl Pts',(-2.09374336261395,-0.372362902338017,
-3.32487045712097));
#6300=CARTESIAN_POINT('Ctrl Pts',(-2.14755530166345,-0.32962253805128,-3.25303157827933));
#6301=CARTESIAN_POINT('Ctrl Pts',(-2.17285695917966,-0.29352982222093,-3.20790907218117));
#6302=CARTESIAN_POINT('Ctrl Pts',(-2.20704841981946,-0.213132057516642,
-3.1398279278523));
#6303=CARTESIAN_POINT('Ctrl Pts',(-2.21822327283998,-0.172744633626709,
-3.11443042987664));
#6304=CARTESIAN_POINT('Ctrl Pts',(-2.23204733756106,-0.0896107157758442,
-3.08209812676733));
#6305=CARTESIAN_POINT('Ctrl Pts',(-2.23547400003843,-0.0488479091023135,
-3.07354689548374));
#6306=CARTESIAN_POINT('Ctrl Pts',(-2.23584472568767,-0.00467961343367746,
-3.07263767088671));
#6307=CARTESIAN_POINT('Ctrl Pts',(-2.23585452428289,-0.00233835250145779,
-3.07261363439072));
#6308=CARTESIAN_POINT('Ctrl Pts',(-2.23585452428289,1.78666159054142E-17,
-3.07261363439072));
#6309=CARTESIAN_POINT('',(-1.54303420125534,-1.06151481751326E-17,-3.47261363439072));
#6310=CARTESIAN_POINT('Ctrl Pts',(-1.54303420125534,-2.77555756156289E-17,
-3.47261363439072));
#6311=CARTESIAN_POINT('Ctrl Pts',(-1.54303420125534,-0.0383517947843985,
-3.47261363439072));
#6312=CARTESIAN_POINT('Ctrl Pts',(-1.54994538759244,-0.0760113765503578,
-3.47360439941826));
#6313=CARTESIAN_POINT('Ctrl Pts',(-1.5808068207282,-0.160957090841637,-3.47744298345925));
#6314=CARTESIAN_POINT('Ctrl Pts',(-1.60922255603095,-0.205137357634195,
-3.48074700181454));
#6315=CARTESIAN_POINT('Ctrl Pts',(-1.68677166592746,-0.289614005670115,
-3.48558093614785));
#6316=CARTESIAN_POINT('Ctrl Pts',(-1.73848860572002,-0.326524134432436,
-3.48650741739372));
#6317=CARTESIAN_POINT('Ctrl Pts',(-1.82831448850183,-0.370775784308151,
-3.47644513959724));
#6318=CARTESIAN_POINT('Ctrl Pts',(-1.86665102369743,-0.384320524321437,
-3.46898747834945));
#6319=CARTESIAN_POINT('Ctrl Pts',(-1.92926064539097,-0.397355586307629,
-3.44733956316554));
#6320=CARTESIAN_POINT('Ctrl Pts',(-1.95331898807439,-0.4,-3.43653534579643));
#6321=CARTESIAN_POINT('Ctrl Pts',(-1.97639320225002,-0.4,-3.42321344203079));
#6322=CARTESIAN_POINT('',(-0.428186507727708,-2.77555756156289E-17,-1.54164078649987));
#6323=CARTESIAN_POINT('',(-0.353589838486224,-4.89858719658941E-17,-1.41243556529821));
#6324=CARTESIAN_POINT('Ctrl Pts',(-0.428186507727708,-2.77555756156289E-17,
-1.54164078649987));
#6325=CARTESIAN_POINT('Ctrl Pts',(-0.428186507727708,0.0504597642713564,
-1.54164078649987));
#6326=CARTESIAN_POINT('Ctrl Pts',(-0.438318998379974,0.1041286832042,-1.53893401838878));
#6327=CARTESIAN_POINT('Ctrl Pts',(-0.478578565558827,0.202612274012173,
-1.52689357905423));
#6328=CARTESIAN_POINT('Ctrl Pts',(-0.508619198410847,0.247446581818911,
-1.5174319796132));
#6329=CARTESIAN_POINT('Ctrl Pts',(-0.576279697432563,0.318233894120627,
-1.49304877698084));
#6330=CARTESIAN_POINT('Ctrl Pts',(-0.61847513021463,0.348984503722909,-1.47646067243115));
#6331=CARTESIAN_POINT('Ctrl Pts',(-0.708513063870763,0.389873348412022,
-1.43542914910365));
#6332=CARTESIAN_POINT('Ctrl Pts',(-0.756306672231996,0.4,-1.41086700060375));
#6333=CARTESIAN_POINT('Ctrl Pts',(-0.843693327768003,0.4,-1.36041429150645));
#6334=CARTESIAN_POINT('Ctrl Pts',(-0.888861576521061,0.389873348412022,
-1.33130488677705));
#6335=CARTESIAN_POINT('Ctrl Pts',(-0.969414884906717,0.348984503722909,
-1.27384551059033));
#6336=CARTESIAN_POINT('Ctrl Pts',(-1.00487832123841,0.318233894120626,-1.24559724615223));
#6337=CARTESIAN_POINT('Ctrl Pts',(-1.05982504365452,0.247446581818911,-1.19919313648287));
#6338=CARTESIAN_POINT('Ctrl Pts',(-1.08303934555689,0.202612274012173,-1.17790798500778));
#6339=CARTESIAN_POINT('Ctrl Pts',(-1.11359645548276,0.1041286832042,-1.1490623967528));
#6340=CARTESIAN_POINT('Ctrl Pts',(-1.12100683075526,0.0504597642713564,
-1.14164078649987));
#6341=CARTESIAN_POINT('Ctrl Pts',(-1.12100683075526,-0.0504597642713564,
-1.14164078649987));
#6342=CARTESIAN_POINT('Ctrl Pts',(-1.11359645548276,-0.1041286832042,-1.1490623967528));
#6343=CARTESIAN_POINT('Ctrl Pts',(-1.08303934555689,-0.202612274012173,
-1.17790798500778));
#6344=CARTESIAN_POINT('Ctrl Pts',(-1.05982504365452,-0.247446581818911,
-1.19919313648287));
#6345=CARTESIAN_POINT('Ctrl Pts',(-1.00487832123841,-0.318233894120626,
-1.24559724615223));
#6346=CARTESIAN_POINT('Ctrl Pts',(-0.969414884906717,-0.348984503722909,
-1.27384551059034));
#6347=CARTESIAN_POINT('Ctrl Pts',(-0.888861576521061,-0.389873348412022,
-1.33130488677705));
#6348=CARTESIAN_POINT('Ctrl Pts',(-0.843693327768003,-0.4,-1.36041429150645));
#6349=CARTESIAN_POINT('Ctrl Pts',(-0.756306672231996,-0.4,-1.41086700060375));
#6350=CARTESIAN_POINT('Ctrl Pts',(-0.708513063870763,-0.389873348412022,
-1.43542914910365));
#6351=CARTESIAN_POINT('Ctrl Pts',(-0.61847513021463,-0.348984503722909,
-1.47646067243115));
#6352=CARTESIAN_POINT('Ctrl Pts',(-0.576279697432563,-0.318233894120627,
-1.49304877698084));
#6353=CARTESIAN_POINT('Ctrl Pts',(-0.508619198410847,-0.247446581818911,
-1.5174319796132));
#6354=CARTESIAN_POINT('Ctrl Pts',(-0.478578565558827,-0.202612274012173,
-1.52689357905423));
#6355=CARTESIAN_POINT('Ctrl Pts',(-0.438318998379974,-0.1041286832042,-1.53893401838878));
#6356=CARTESIAN_POINT('Ctrl Pts',(-0.428186507727708,-0.0504597642713564,
-1.54164078649987));
#6357=CARTESIAN_POINT('Ctrl Pts',(-0.428186507727708,0.,-1.54164078649987));
#6358=CARTESIAN_POINT('Ctrl Pts',(-2.23585452428289,7.63278329429795E-17,
-3.07261363439072));
#6359=CARTESIAN_POINT('Ctrl Pts',(-2.23585452428289,0.0410730673371933,
-3.07261363439072));
#6360=CARTESIAN_POINT('Ctrl Pts',(-2.23288112519932,0.0812488103420015,
-3.08004754625334));
#6361=CARTESIAN_POINT('Ctrl Pts',(-2.2194892520593,0.168643605332515,-3.11157416462442));
#6362=CARTESIAN_POINT('Ctrl Pts',(-2.20746489927147,0.212871126833592,-3.13916711480983));
#6363=CARTESIAN_POINT('Ctrl Pts',(-2.17432971862124,0.289288653612542,-3.20479413071362));
#6364=CARTESIAN_POINT('Ctrl Pts',(-2.15299432784447,0.321562705912151,-3.24321359311856));
#6365=CARTESIAN_POINT('Ctrl Pts',(-2.10385766863634,0.366289871498909,-3.31269862563671));
#6366=CARTESIAN_POINT('Ctrl Pts',(-2.07763067369275,0.381582813899271,-3.34420417049112));
#6367=CARTESIAN_POINT('Ctrl Pts',(-2.02649549880538,0.396376989861723,-3.39007664729581));
#6368=CARTESIAN_POINT('Ctrl Pts',(-2.00500851837093,0.399534030132352,-3.40615678433065));
#6369=CARTESIAN_POINT('Ctrl Pts',(-1.95915250835263,0.400357587283029,-3.43357837117363));
#6370=CARTESIAN_POINT('Ctrl Pts',(-1.93562848585123,0.398184081632146,-3.44461877107984));
#6371=CARTESIAN_POINT('Ctrl Pts',(-1.875434536778,0.386733579315055,-3.46656089746854));
#6372=CARTESIAN_POINT('Ctrl Pts',(-1.83900843587021,0.374717415049472,-3.47443089530928));
#6373=CARTESIAN_POINT('Ctrl Pts',(-1.75086673562183,0.334141370748251,-3.48605931114578));
#6374=CARTESIAN_POINT('Ctrl Pts',(-1.69897284605408,0.29919347125353,-3.48584718519127));
#6375=CARTESIAN_POINT('Ctrl Pts',(-1.62110766869098,0.220248198730226,-3.48177873127923));
#6376=CARTESIAN_POINT('Ctrl Pts',(-1.59225272572432,0.179861222706076,-3.47871239651179));
#6377=CARTESIAN_POINT('Ctrl Pts',(-1.55528921655549,0.0967734525439036,
-3.47434740697038));
#6378=CARTESIAN_POINT('Ctrl Pts',(-1.545215709166,0.0560978356893791,-3.47291284339176));
#6379=CARTESIAN_POINT('Ctrl Pts',(-1.54313901012609,0.00945212461834998,
-3.47262803946294));
#6380=CARTESIAN_POINT('Ctrl Pts',(-1.54303420125534,0.00472081811281199,
-3.47261363439072));
#6381=CARTESIAN_POINT('Ctrl Pts',(-1.54303420125534,-1.73503143864141E-18,
-3.47261363439072));
#6382=CARTESIAN_POINT('Origin',(1.4,0.,0.));
#6383=CARTESIAN_POINT('',(3.95278640450004,-0.4,-2.35922392732846E-16));
#6384=CARTESIAN_POINT('',(3.77888872553824,1.09597789965446E-16,-0.4));
#6385=CARTESIAN_POINT('Ctrl Pts',(3.95278640450004,-0.4,-2.35922392732846E-16));
#6386=CARTESIAN_POINT('Ctrl Pts',(3.95278640450004,-0.4,-0.0258360862047648));
#6387=CARTESIAN_POINT('Ctrl Pts',(3.95027516460594,-0.397512833149891,-0.0512701351527404));
#6388=CARTESIAN_POINT('Ctrl Pts',(3.9368973062695,-0.383653411095849,-0.122687402596185));
#6389=CARTESIAN_POINT('Ctrl Pts',(3.92099313571869,-0.366726070737926,-0.165860440942593));
#6390=CARTESIAN_POINT('Ctrl Pts',(3.88215383386439,-0.31747069067207,-0.248777381546757));
#6391=CARTESIAN_POINT('Ctrl Pts',(3.85821727363502,-0.282645638038343,-0.287806205063065));
#6392=CARTESIAN_POINT('Ctrl Pts',(3.81778817347559,-0.202263253170223,-0.348492766284571));
#6393=CARTESIAN_POINT('Ctrl Pts',(3.80079075477909,-0.157459904108683,-0.37127224556947));
#6394=CARTESIAN_POINT('Ctrl Pts',(3.78287958748677,-0.0731574180396009,
-0.394916332862525));
#6395=CARTESIAN_POINT('Ctrl Pts',(3.77888872553824,-0.0369000545189914,
-0.4));
#6396=CARTESIAN_POINT('Ctrl Pts',(3.77888872553824,1.94289029309402E-16,
-0.4));
#6397=CARTESIAN_POINT('',(3.77888872553824,-5.39832350745528E-17,0.4));
#6398=CARTESIAN_POINT('Ctrl Pts',(3.77888872553824,-1.17961196366423E-16,
0.4));
#6399=CARTESIAN_POINT('Ctrl Pts',(3.77888872553824,-0.0272727676506818,
0.4));
#6400=CARTESIAN_POINT('Ctrl Pts',(3.78106300168282,-0.0544020323932614,
0.397217418228499));
#6401=CARTESIAN_POINT('Ctrl Pts',(3.79271825761897,-0.127937297231108,0.381999133565693));
#6402=CARTESIAN_POINT('Ctrl Pts',(3.80621018335175,-0.171414515873833,0.36427330945719));
#6403=CARTESIAN_POINT('Ctrl Pts',(3.84417532906779,-0.259603664828111,0.309803247199999));
#6404=CARTESIAN_POINT('Ctrl Pts',(3.87017758215935,-0.300373167337263,0.269798321919243));
#6405=CARTESIAN_POINT('Ctrl Pts',(3.91068088989223,-0.354517112418169,0.189870142116222));
#6406=CARTESIAN_POINT('Ctrl Pts',(3.92708058985812,-0.372975101147337,0.151019887329265));
#6407=CARTESIAN_POINT('Ctrl Pts',(3.94744069529494,-0.394767506762619,0.0739864326554591));
#6408=CARTESIAN_POINT('Ctrl Pts',(3.95278640450004,-0.4,0.037557140405018));
#6409=CARTESIAN_POINT('Ctrl Pts',(3.95278640450004,-0.4,-2.42861286636753E-16));
#6410=CARTESIAN_POINT('',(1.54919333848297,-1.38777878078145E-17,0.4));
#6411=CARTESIAN_POINT('',(1.4,-4.89858719658941E-17,0.4));
#6412=CARTESIAN_POINT('Ctrl Pts',(1.54919333848297,-1.38777878078145E-17,
0.4));
#6413=CARTESIAN_POINT('Ctrl Pts',(1.54919333848297,0.0504597642713564,0.4));
#6414=CARTESIAN_POINT('Ctrl Pts',(1.55191545386274,0.1041286832042,0.389871621635982));
#6415=CARTESIAN_POINT('Ctrl Pts',(1.56161791111572,0.202612274012173,0.348985594046454));
#6416=CARTESIAN_POINT('Ctrl Pts',(1.56844424206536,0.247446581818911,0.318238843130327));
#6417=CARTESIAN_POINT('Ctrl Pts',(1.58115801867098,0.318233894120626,0.247451530828612));
#6418=CARTESIAN_POINT('Ctrl Pts',(1.58789001512135,0.348984503722909,0.202615161840818));
#6419=CARTESIAN_POINT('Ctrl Pts',(1.59737464039182,0.389873348412022,0.104124262326598));
#6420=CARTESIAN_POINT('Ctrl Pts',(1.6,0.4,0.0504527090972947));
#6421=CARTESIAN_POINT('Ctrl Pts',(1.6,0.4,-0.0504527090972948));
#6422=CARTESIAN_POINT('Ctrl Pts',(1.59737464039182,0.389873348412022,-0.104124262326598));
#6423=CARTESIAN_POINT('Ctrl Pts',(1.58789001512135,0.348984503722909,-0.202615161840818));
#6424=CARTESIAN_POINT('Ctrl Pts',(1.58115801867098,0.318233894120626,-0.247451530828612));
#6425=CARTESIAN_POINT('Ctrl Pts',(1.56844424206536,0.247446581818911,-0.318238843130327));
#6426=CARTESIAN_POINT('Ctrl Pts',(1.56161791111572,0.202612274012173,-0.348985594046454));
#6427=CARTESIAN_POINT('Ctrl Pts',(1.55191545386274,0.1041286832042,-0.389871621635982));
#6428=CARTESIAN_POINT('Ctrl Pts',(1.54919333848297,0.0504597642713565,-0.4));
#6429=CARTESIAN_POINT('Ctrl Pts',(1.54919333848297,-0.0504597642713564,
-0.4));
#6430=CARTESIAN_POINT('Ctrl Pts',(1.55191545386274,-0.1041286832042,-0.389871621635982));
#6431=CARTESIAN_POINT('Ctrl Pts',(1.56161791111572,-0.202612274012173,-0.348985594046454));
#6432=CARTESIAN_POINT('Ctrl Pts',(1.56844424206536,-0.247446581818911,-0.318238843130327));
#6433=CARTESIAN_POINT('Ctrl Pts',(1.58115801867098,-0.318233894120626,-0.247451530828612));
#6434=CARTESIAN_POINT('Ctrl Pts',(1.58789001512135,-0.348984503722909,-0.202615161840818));
#6435=CARTESIAN_POINT('Ctrl Pts',(1.59737464039182,-0.389873348412022,-0.104124262326598));
#6436=CARTESIAN_POINT('Ctrl Pts',(1.6,-0.4,-0.0504527090972948));
#6437=CARTESIAN_POINT('Ctrl Pts',(1.6,-0.4,0.0504527090972947));
#6438=CARTESIAN_POINT('Ctrl Pts',(1.59737464039182,-0.389873348412022,0.104124262326598));
#6439=CARTESIAN_POINT('Ctrl Pts',(1.58789001512135,-0.348984503722909,0.202615161840818));
#6440=CARTESIAN_POINT('Ctrl Pts',(1.58115801867098,-0.318233894120626,0.247451530828612));
#6441=CARTESIAN_POINT('Ctrl Pts',(1.56844424206536,-0.247446581818911,0.318238843130327));
#6442=CARTESIAN_POINT('Ctrl Pts',(1.56161791111572,-0.202612274012173,0.348985594046454));
#6443=CARTESIAN_POINT('Ctrl Pts',(1.55191545386274,-0.1041286832042,0.389871621635982));
#6444=CARTESIAN_POINT('Ctrl Pts',(1.54919333848297,-0.0504597642713564,
0.4));
#6445=CARTESIAN_POINT('Ctrl Pts',(1.54919333848297,-1.38777878078145E-17,
0.4));
#6446=CARTESIAN_POINT('Ctrl Pts',(3.77888872553824,1.86829229348027E-16,
-0.4));
#6447=CARTESIAN_POINT('Ctrl Pts',(3.77888872553824,0.00309498603048382,
-0.4));
#6448=CARTESIAN_POINT('Ctrl Pts',(3.77891661019551,0.00619449342134284,
-0.399964080504009));
#6449=CARTESIAN_POINT('Ctrl Pts',(3.77971687905484,0.0505413576531444,-0.398932950425445));
#6450=CARTESIAN_POINT('Ctrl Pts',(3.78543557857047,0.0907018003769345,-0.391648799570242));
#6451=CARTESIAN_POINT('Ctrl Pts',(3.80769137218302,0.178071320347422,-0.361944214113905));
#6452=CARTESIAN_POINT('Ctrl Pts',(3.82654127450702,0.222292530416346,-0.336211120851667));
#6453=CARTESIAN_POINT('Ctrl Pts',(3.86943599025501,0.300322258788604,-0.269500799758935));
#6454=CARTESIAN_POINT('Ctrl Pts',(3.89351725477811,0.332784356169053,-0.227832272860913));
#6455=CARTESIAN_POINT('Ctrl Pts',(3.92736856657203,0.373587746906379,-0.147954668532213));
#6456=CARTESIAN_POINT('Ctrl Pts',(3.93961646455397,0.386498097215894,-0.110669509456768));
#6457=CARTESIAN_POINT('Ctrl Pts',(3.95306292785875,0.400371072665748,-0.0337021304926297));
#6458=CARTESIAN_POINT('Ctrl Pts',(3.9545592908845,0.401808180012853,0.00409487952092722));
#6459=CARTESIAN_POINT('Ctrl Pts',(3.94603596920218,0.393166016942161,0.0855981766489427));
#6460=CARTESIAN_POINT('Ctrl Pts',(3.93468925406179,0.381660209981968,0.126674111541842));
#6461=CARTESIAN_POINT('Ctrl Pts',(3.90112046658193,0.342583173264719,0.213361732985292));
#6462=CARTESIAN_POINT('Ctrl Pts',(3.87621280158359,0.310552040291197,0.258074179286464));
#6463=CARTESIAN_POINT('Ctrl Pts',(3.83422313437239,0.237524054838919,0.324800962724505));
#6464=CARTESIAN_POINT('Ctrl Pts',(3.81668267570578,0.199892119948508,0.349479486409192));
#6465=CARTESIAN_POINT('Ctrl Pts',(3.79128132597323,0.119375494000328,0.38406200828837));
#6466=CARTESIAN_POINT('Ctrl Pts',(3.78294965429021,0.0778792943511222,0.39475779223555));
#6467=CARTESIAN_POINT('Ctrl Pts',(3.77927203108033,0.0229673800676086,0.39950680005141));
#6468=CARTESIAN_POINT('Ctrl Pts',(3.77888872553824,0.011470996564166,0.4));
#6469=CARTESIAN_POINT('Ctrl Pts',(3.77888872553824,-9.36750677027476E-17,
0.4));
#6470=CARTESIAN_POINT('Origin',(1.6,1.9,0.));
#6471=CARTESIAN_POINT('',(-1.6,1.9,-1.95943487863577E-16));
#6472=CARTESIAN_POINT('Origin',(0.,1.9,0.));
#6473=CARTESIAN_POINT('Origin',(0.,0.,0.));
#6474=CARTESIAN_POINT('',(-1.6,0.,-1.95943487863577E-16));
#6475=CARTESIAN_POINT('',(-1.6,0.,-1.95943487863577E-16));
#6476=CARTESIAN_POINT('Origin',(0.,0.,0.));
#6477=CARTESIAN_POINT('',(-4.65365783675994E-16,-7.34788079488412E-17,3.8));
#6478=CARTESIAN_POINT('Origin',(-5.38844591624835E-16,0.,4.4));
#6479=CARTESIAN_POINT('Origin',(0.,7.34788079488412E-17,0.));
#6480=CARTESIAN_POINT('Origin',(0.,7.34788079488412E-17,0.));
#6481=CARTESIAN_POINT('Origin',(0.,7.34788079488412E-17,0.));
#6482=CARTESIAN_POINT('Origin',(0.,7.34788079488412E-17,0.));
#6483=CARTESIAN_POINT('',(0.,0.,0.));
#6774=UNCERTAINTY_MEASURE_WITH_UNIT(LENGTH_MEASURE(0.001),#6806,
'DISTANCE_ACCURACY_VALUE',
'Maximum model space distance between geometric entities at asserted c
onnectivities');
#6780=UNCERTAINTY_MEASURE_WITH_UNIT(LENGTH_MEASURE(0.001),#6806,
'DISTANCE_ACCURACY_VALUE',
'Maximum model space distance between geometric entities at asserted c
onnectivities');
#6799=(
GEOMETRIC_REPRESENTATION_CONTEXT(3)
GLOBAL_UNCERTAINTY_ASSIGNED_CONTEXT((#6774))
GLOBAL_UNIT_ASSIGNED_CONTEXT((#6806,#6808,#6809))
REPRESENTATION_CONTEXT('','3D')
);
#6805=(
GEOMETRIC_REPRESENTATION_CONTEXT(3)
GLOBAL_UNCERTAINTY_ASSIGNED_CONTEXT((#6780))
GLOBAL_UNIT_ASSIGNED_CONTEXT((#6806,#6808,#6809))
REPRESENTATION_CONTEXT('','3D')
);
#6806=(
LENGTH_UNIT()
NAMED_UNIT(*)
SI_UNIT(.CENTI.,.METRE.)
);
#6808=(
NAMED_UNIT(*)
PLANE_ANGLE_UNIT()
SI_UNIT($,.RADIAN.)
);
#6809=(
NAMED_UNIT(*)
SI_UNIT($,.STERADIAN.)
SOLID_ANGLE_UNIT()
);
#6828=SHAPE_DEFINITION_REPRESENTATION(#6881,#6916);
#6881=PRODUCT_DEFINITION_SHAPE('',$,#6941);
#6916=SHAPE_REPRESENTATION('',(#3819,#3854),#6799);
#6922=PRODUCT_DEFINITION_CONTEXT('part definition',#6996,'design');
#6941=PRODUCT_DEFINITION('Handwheel - 100 mm Diameter, 12 mm Bore',
'Handwheel - 100 mm Diameter, 12 mm Bore',#6965,#6922);
#6965=PRODUCT_DEFINITION_FORMATION('',$,#7016);
#6996=APPLICATION_CONTEXT(
'Core Data for Automotive Mechanical Design Process');
#6997=PRODUCT_CONTEXT('part definition',#6996,'mechanical');
#7016=PRODUCT('Handwheel - 100 mm Diameter, 12 mm Bore',
'Handwheel - 100 mm Diameter, 12 mm Bore',
'Handwheel - 100 mm Diameter, 12 mm Bore',(#6997));
#7078=COLOUR_RGB('Sky Blue',0.24,0.69,0.87);
#7079=FILL_AREA_STYLE_COLOUR('',#7078);
#7080=FILL_AREA_STYLE('',(#7079));
#7081=SURFACE_STYLE_FILL_AREA(#7080);
#7082=SURFACE_SIDE_STYLE('',(#7081));
#7083=SURFACE_STYLE_USAGE(.BOTH.,#7082);
#7084=PRESENTATION_STYLE_ASSIGNMENT((#7083));
ENDSEC;
END-ISO-10303-21;
